ISO-10303-21;
HEADER;
/* Generated by software containing ST-Developer
 * from STEP Tools, Inc. (www.steptools.com) 
 */

FILE_DESCRIPTION(
/* description */ ('Independent hinged machine back cover with retained hinge pins, perim
eter gasket and quarter-turn cam latch. Nominal cover 360 x 260 x 3 mm
, frame 430 x 300 x 20 mm. No guarding, structural or ingress rating a
ssigned.'),
/* implementation_level */ '2;1');

FILE_NAME(
/* name */ 'Hex nut M6.step',
/* time_stamp */ '2026-11-09T19:36:59-08:00',
/* author */ (''),
/* organization */ (''),
/* preprocessor_version */ 'ST-DEVELOPER v20.2',
/* originating_system */ 'Autodesk Translation Framework v15.17.0.0',
/* authorisation */ '');

FILE_SCHEMA (('AUTOMOTIVE_DESIGN { 1 0 10303 214 3 1 1 }'));
ENDSEC;

DATA;
#10=MECHANICAL_DESIGN_GEOMETRIC_PRESENTATION_REPRESENTATION('',(#215),#32627);
#179=SHAPE_REPRESENTATION_RELATIONSHIP('SRR','None',#32725,#197);
#197=ADVANCED_BREP_SHAPE_REPRESENTATION('',(#233),#32626);
#215=STYLED_ITEM('',(#32810),#233);
#233=MANIFOLD_SOLID_BREP('Body1',#8692);
#291=FACE_BOUND('',#1451,.T.);
#292=FACE_BOUND('',#1460,.T.);
#309=B_SPLINE_SURFACE_WITH_KNOTS('',3,3,((#31802,#31803,#31804,#31805,#31806,
#31807,#31808,#31809,#31810,#31811,#31812,#31813,#31814,#31815,#31816,#31817,
#31818,#31819,#31820,#31821,#31822,#31823,#31824,#31825,#31826,#31827,#31828,
#31829,#31830,#31831,#31832,#31833,#31834,#31835,#31836,#31837,#31838),
(#31839,#31840,#31841,#31842,#31843,#31844,#31845,#31846,#31847,#31848,
#31849,#31850,#31851,#31852,#31853,#31854,#31855,#31856,#31857,#31858,#31859,
#31860,#31861,#31862,#31863,#31864,#31865,#31866,#31867,#31868,#31869,#31870,
#31871,#31872,#31873,#31874,#31875),(#31876,#31877,#31878,#31879,#31880,
#31881,#31882,#31883,#31884,#31885,#31886,#31887,#31888,#31889,#31890,#31891,
#31892,#31893,#31894,#31895,#31896,#31897,#31898,#31899,#31900,#31901,#31902,
#31903,#31904,#31905,#31906,#31907,#31908,#31909,#31910,#31911,#31912),
(#31913,#31914,#31915,#31916,#31917,#31918,#31919,#31920,#31921,#31922,
#31923,#31924,#31925,#31926,#31927,#31928,#31929,#31930,#31931,#31932,#31933,
#31934,#31935,#31936,#31937,#31938,#31939,#31940,#31941,#31942,#31943,#31944,
#31945,#31946,#31947,#31948,#31949)),.UNSPECIFIED.,.F.,.F.,.F.,(4,4),(4,
1,1,1,1,1,1,1,1,1,1,1,1,1,1,1,1,1,1,1,1,1,1,1,1,1,1,1,1,1,1,1,1,1,4),(0.,
0.0642013499338864),(11.8589888623078,12.8423086102174,13.825628358127,
14.8089481060366,15.7922678539462,16.7755876018558,17.7589073497654,18.742227097675,
19.7255468455846,20.7088665934942,21.6921863414038,22.6755060893134,23.658825837223,
24.6421455851326,25.6254653330422,26.6087850809518,27.5921048288614,28.575424576771,
29.5587443246806,30.5420640725902,31.5253838204998,32.5087035684094,33.492023316319,
34.4753430642286,35.4586628121382,36.4419825600478,37.4253023079574,38.408622055867,
39.3919418037766,40.3752615516862,41.3585812995958,42.3419010475054,43.325220795415,
44.3085405433246,45.2918602912342),.UNSPECIFIED.);
#310=B_SPLINE_SURFACE_WITH_KNOTS('',3,3,((#32157,#32158,#32159,#32160,#32161,
#32162,#32163,#32164,#32165,#32166,#32167,#32168,#32169,#32170,#32171,#32172,
#32173,#32174,#32175,#32176,#32177,#32178,#32179,#32180,#32181,#32182,#32183,
#32184,#32185,#32186,#32187,#32188,#32189,#32190,#32191,#32192,#32193),
(#32194,#32195,#32196,#32197,#32198,#32199,#32200,#32201,#32202,#32203,
#32204,#32205,#32206,#32207,#32208,#32209,#32210,#32211,#32212,#32213,#32214,
#32215,#32216,#32217,#32218,#32219,#32220,#32221,#32222,#32223,#32224,#32225,
#32226,#32227,#32228,#32229,#32230),(#32231,#32232,#32233,#32234,#32235,
#32236,#32237,#32238,#32239,#32240,#32241,#32242,#32243,#32244,#32245,#32246,
#32247,#32248,#32249,#32250,#32251,#32252,#32253,#32254,#32255,#32256,#32257,
#32258,#32259,#32260,#32261,#32262,#32263,#32264,#32265,#32266,#32267),
(#32268,#32269,#32270,#32271,#32272,#32273,#32274,#32275,#32276,#32277,
#32278,#32279,#32280,#32281,#32282,#32283,#32284,#32285,#32286,#32287,#32288,
#32289,#32290,#32291,#32292,#32293,#32294,#32295,#32296,#32297,#32298,#32299,
#32300,#32301,#32302,#32303,#32304)),.UNSPECIFIED.,.F.,.F.,.F.,(4,4),(4,
1,1,1,1,1,1,1,1,1,1,1,1,1,1,1,1,1,1,1,1,1,1,1,1,1,1,1,1,1,1,1,1,1,4),(0.,
0.0642013499338863),(14.3984001269719,15.3817198748815,16.3650396227911,
17.3483593707007,18.3316791186103,19.3149988665199,20.2983186144295,21.2816383623391,
22.2649581102487,23.2482778581583,24.2315976060679,25.2149173539775,26.1982371018871,
27.1815568497966,28.1648765977063,29.1481963456159,30.1315160935254,31.114835841435,
32.0981555893446,33.0814753372542,34.0647950851639,35.0481148330734,36.031434580983,
37.0147543288926,37.9980740768022,38.9813938247118,39.9647135726214,40.948033320531,
41.9313530684406,42.9146728163502,43.8979925642598,44.8813123121694,45.864632060079,
46.8479518079886,47.8312715558982),.UNSPECIFIED.);
#444=PLANE('',#9483);
#445=PLANE('',#9485);
#446=PLANE('',#9486);
#447=PLANE('',#9487);
#448=PLANE('',#9488);
#449=PLANE('',#9489);
#450=PLANE('',#9490);
#451=PLANE('',#9491);
#905=FACE_OUTER_BOUND('',#1437,.T.);
#906=FACE_OUTER_BOUND('',#1438,.T.);
#907=FACE_OUTER_BOUND('',#1439,.T.);
#908=FACE_OUTER_BOUND('',#1440,.T.);
#909=FACE_OUTER_BOUND('',#1441,.T.);
#910=FACE_OUTER_BOUND('',#1442,.T.);
#911=FACE_OUTER_BOUND('',#1443,.T.);
#912=FACE_OUTER_BOUND('',#1444,.T.);
#913=FACE_OUTER_BOUND('',#1445,.T.);
#914=FACE_OUTER_BOUND('',#1446,.T.);
#915=FACE_OUTER_BOUND('',#1447,.T.);
#916=FACE_OUTER_BOUND('',#1448,.T.);
#917=FACE_OUTER_BOUND('',#1449,.T.);
#918=FACE_OUTER_BOUND('',#1450,.T.);
#919=FACE_OUTER_BOUND('',#1452,.T.);
#920=FACE_OUTER_BOUND('',#1453,.T.);
#921=FACE_OUTER_BOUND('',#1454,.T.);
#922=FACE_OUTER_BOUND('',#1455,.T.);
#923=FACE_OUTER_BOUND('',#1456,.T.);
#924=FACE_OUTER_BOUND('',#1457,.T.);
#925=FACE_OUTER_BOUND('',#1458,.T.);
#926=FACE_OUTER_BOUND('',#1459,.T.);
#1437=EDGE_LOOP('',(#7767,#7768,#7769,#7770));
#1438=EDGE_LOOP('',(#7771,#7772,#7773,#7774));
#1439=EDGE_LOOP('',(#7775,#7776,#7777,#7778));
#1440=EDGE_LOOP('',(#7779,#7780,#7781,#7782));
#1441=EDGE_LOOP('',(#7783,#7784,#7785,#7786));
#1442=EDGE_LOOP('',(#7787,#7788,#7789,#7790));
#1443=EDGE_LOOP('',(#7791,#7792,#7793,#7794));
#1444=EDGE_LOOP('',(#7795,#7796,#7797,#7798));
#1445=EDGE_LOOP('',(#7799,#7800,#7801,#7802));
#1446=EDGE_LOOP('',(#7803,#7804,#7805,#7806));
#1447=EDGE_LOOP('',(#7807,#7808,#7809,#7810));
#1448=EDGE_LOOP('',(#7811,#7812,#7813,#7814,#7815,#7816,#7817,#7818,#7819,
#7820,#7821,#7822,#7823,#7824));
#1449=EDGE_LOOP('',(#7825,#7826,#7827,#7828,#7829,#7830,#7831,#7832,#7833,
#7834,#7835,#7836,#7837,#7838));
#1450=EDGE_LOOP('',(#7839,#7840,#7841,#7842,#7843,#7844));
#1451=EDGE_LOOP('',(#7845,#7846,#7847,#7848));
#1452=EDGE_LOOP('',(#7849,#7850,#7851,#7852));
#1453=EDGE_LOOP('',(#7853,#7854,#7855,#7856));
#1454=EDGE_LOOP('',(#7857,#7858,#7859,#7860));
#1455=EDGE_LOOP('',(#7861,#7862,#7863,#7864));
#1456=EDGE_LOOP('',(#7865,#7866,#7867,#7868));
#1457=EDGE_LOOP('',(#7869,#7870,#7871,#7872));
#1458=EDGE_LOOP('',(#7873,#7874,#7875,#7876));
#1459=EDGE_LOOP('',(#7877,#7878,#7879,#7880,#7881,#7882));
#1460=EDGE_LOOP('',(#7883,#7884,#7885,#7886));
#1581=CIRCLE('',#9469,2.5175);
#1582=CIRCLE('',#9474,2.5175);
#1583=CIRCLE('',#9476,3.0735);
#1584=CIRCLE('',#9481,3.0735);
#2147=B_SPLINE_CURVE_WITH_KNOTS('',3,(#31460,#31461,#31462,#31463),
 .UNSPECIFIED.,.F.,.F.,(4,4),(32.725489676875,33.4328714289264),
 .UNSPECIFIED.);
#2148=B_SPLINE_CURVE_WITH_KNOTS('',3,(#31466,#31467,#31468,#31469,#31470,
#31471,#31472,#31473,#31474,#31475),.UNSPECIFIED.,.F.,.F.,(4,3,3,4),(-31.4159265358979,
-30.4829121851976,-29.499592437288,-28.9817156343595),.UNSPECIFIED.);
#2149=B_SPLINE_CURVE_WITH_KNOTS('',3,(#31480,#31481,#31482,#31483,#31484,
#31485,#31486,#31487,#31488,#31489,#31490,#31491,#31492,#31493,#31494,#31495,
#31496,#31497,#31498,#31499,#31500,#31501,#31502,#31503,#31504),
 .UNSPECIFIED.,.F.,.F.,(4,3,3,3,3,3,3,3,4),(26.4423043696954,26.5496331935592,
27.5329529414688,28.5162726893784,29.499592437288,30.4829121851976,31.4662319331072,
32.4495516810168,32.725489676875),.UNSPECIFIED.);
#2150=B_SPLINE_CURVE_WITH_KNOTS('',3,(#31505,#31506,#31507,#31508,#31509,
#31510,#31511,#31512,#31513,#31514,#31515,#31516,#31517,#31518,#31519,#31520,
#31521,#31522,#31523,#31524,#31525,#31526),.UNSPECIFIED.,.F.,.F.,(4,3,3,
3,3,3,3,4),(-28.9817156343595,-28.5162726893784,-27.5329529414688,-26.5496331935592,
-25.5663134456496,-24.58299369774,-23.5996739498304,-22.6985303271799),
 .UNSPECIFIED.);
#2151=B_SPLINE_CURVE_WITH_KNOTS('',3,(#31531,#31532,#31533,#31534,#31535,
#31536,#31537,#31538,#31539,#31540,#31541,#31542,#31543,#31544,#31545,#31546,
#31547,#31548,#31549,#31550,#31551,#31552),.UNSPECIFIED.,.F.,.F.,(4,3,3,
3,3,3,3,4),(20.1591190625159,20.6497147061016,21.6330344540112,22.6163542019208,
23.5996739498304,24.58299369774,25.5663134456496,26.4423043696954),
 .UNSPECIFIED.);
#2152=B_SPLINE_CURVE_WITH_KNOTS('',3,(#31553,#31554,#31555,#31556,#31557,
#31558,#31559,#31560,#31561,#31562,#31563,#31564,#31565,#31566,#31567,#31568,
#31569,#31570,#31571,#31572,#31573,#31574,#31575,#31576,#31577),
 .UNSPECIFIED.,.F.,.F.,(4,3,3,3,3,3,3,3,4),(-22.6985303271799,-22.6163542019208,
-21.6330344540112,-20.6497147061016,-19.666394958192,-18.6830752102824,
-17.6997554623728,-16.7164357144632,-16.4153450200003),.UNSPECIFIED.);
#2153=B_SPLINE_CURVE_WITH_KNOTS('',3,(#31582,#31583,#31584,#31585,#31586,
#31587,#31588,#31589,#31590,#31591,#31592,#31593,#31594,#31595,#31596,#31597,
#31598,#31599,#31600,#31601,#31602,#31603),.UNSPECIFIED.,.F.,.F.,(4,3,3,
3,3,3,3,4),(13.8759337553363,14.749796218644,15.7331159665536,16.7164357144632,
17.6997554623728,18.6830752102824,19.666394958192,20.1591190625159),
 .UNSPECIFIED.);
#2154=B_SPLINE_CURVE_WITH_KNOTS('',3,(#31604,#31605,#31606,#31607,#31608,
#31609,#31610,#31611,#31612,#31613,#31614,#31615,#31616,#31617,#31618,#31619,
#31620,#31621,#31622,#31623,#31624,#31625),.UNSPECIFIED.,.F.,.F.,(4,3,3,
3,3,3,3,4),(-16.4153450200003,-15.7331159665536,-14.749796218644,-13.7664764707344,
-12.7831567228248,-11.7998369749152,-10.8165172270056,-10.1321597128207),
 .UNSPECIFIED.);
#2155=B_SPLINE_CURVE_WITH_KNOTS('',3,(#31631,#31632,#31633,#31634,#31635,
#31636,#31637,#31638,#31639,#31640,#31641,#31642,#31643),.UNSPECIFIED.,
 .F.,.F.,(4,3,3,3,4),(-3.84897440564114,-2.9499592437288,-1.9666394958192,
-0.983319747909601,0.),.UNSPECIFIED.);
#2156=B_SPLINE_CURVE_WITH_KNOTS('',3,(#31646,#31647,#31648,#31649,#31650,
#31651,#31652,#31653,#31654,#31655,#31656,#31657,#31658,#31659,#31660,#31661,
#31662,#31663,#31664),.UNSPECIFIED.,.F.,.F.,(4,3,3,3,3,3,4),(2.01694489302844,
2.9499592437288,3.9332789916384,4.916598739548,5.8999184874576,6.8832382353672,
7.59274844815668),.UNSPECIFIED.);
#2157=B_SPLINE_CURVE_WITH_KNOTS('',3,(#31670,#31671,#31672,#31673,#31674,
#31675,#31676,#31677),.UNSPECIFIED.,.F.,.F.,(4,1,1,1,1,4),(40.8407044966673,
41.3585812995958,42.3419010475054,43.325220795415,44.3085405433246,45.2918602912342),
 .UNSPECIFIED.);
#2158=B_SPLINE_CURVE_WITH_KNOTS('',3,(#31680,#31681,#31682,#31683,#31684,
#31685,#31686,#31687,#31688),.UNSPECIFIED.,.F.,.F.,(4,1,1,1,1,1,4),(40.8407044966673,
40.948033320531,41.9313530684406,42.9146728163502,43.8979925642598,44.8813123121694,
45.8143266628698),.UNSPECIFIED.);
#2159=B_SPLINE_CURVE_WITH_KNOTS('',3,(#31693,#31694,#31695,#31696,#31697,
#31698,#31699,#31700,#31701,#31702),.UNSPECIFIED.,.F.,.F.,(4,1,1,1,1,1,
1,4),(34.5575191894877,35.4586628121382,36.4419825600478,37.4253023079574,
38.408622055867,39.3919418037766,40.3752615516862,40.8407044966673),
 .UNSPECIFIED.);
#2160=B_SPLINE_CURVE_WITH_KNOTS('',3,(#31703,#31704,#31705,#31706,#31707,
#31708,#31709,#31710,#31711,#31712),.UNSPECIFIED.,.F.,.F.,(4,1,1,1,1,1,
1,4),(34.5575191894877,35.0481148330734,36.031434580983,37.0147543288926,
37.9980740768022,38.9813938247118,39.9647135726214,40.8407044966673),
 .UNSPECIFIED.);
#2161=B_SPLINE_CURVE_WITH_KNOTS('',3,(#31717,#31718,#31719,#31720,#31721,
#31722,#31723,#31724,#31725,#31726,#31727),.UNSPECIFIED.,.F.,.F.,(4,1,1,
1,1,1,1,1,4),(28.2743338823081,28.575424576771,29.5587443246806,30.5420640725902,
31.5253838204998,32.5087035684094,33.492023316319,34.4753430642286,34.5575191894877),
 .UNSPECIFIED.);
#2162=B_SPLINE_CURVE_WITH_KNOTS('',3,(#31728,#31729,#31730,#31731,#31732,
#31733,#31734,#31735,#31736,#31737),.UNSPECIFIED.,.F.,.F.,(4,1,1,1,1,1,
1,4),(28.2743338823081,29.1481963456159,30.1315160935254,31.114835841435,
32.0981555893446,33.0814753372542,34.0647950851639,34.5575191894877),
 .UNSPECIFIED.);
#2163=B_SPLINE_CURVE_WITH_KNOTS('',3,(#31742,#31743,#31744,#31745,#31746,
#31747,#31748,#31749,#31750,#31751),.UNSPECIFIED.,.F.,.F.,(4,1,1,1,1,1,
1,4),(21.9911485751285,22.6755060893134,23.658825837223,24.6421455851326,
25.6254653330422,26.6087850809518,27.5921048288614,28.2743338823081),
 .UNSPECIFIED.);
#2164=B_SPLINE_CURVE_WITH_KNOTS('',3,(#31752,#31753,#31754,#31755,#31756,
#31757,#31758,#31759,#31760,#31761,#31762),.UNSPECIFIED.,.F.,.F.,(4,1,1,
1,1,1,1,1,4),(21.9911485751285,22.2649581102487,23.2482778581583,24.2315976060679,
25.2149173539775,26.1982371018871,27.1815568497966,28.1648765977063,28.2743338823081),
 .UNSPECIFIED.);
#2165=B_SPLINE_CURVE_WITH_KNOTS('',3,(#31768,#31769,#31770,#31771,#31772),
 .UNSPECIFIED.,.F.,.F.,(4,1,4),(14.3984001269719,15.3817198748815,15.7079632679489),
 .UNSPECIFIED.);
#2166=B_SPLINE_CURVE_WITH_KNOTS('',3,(#31775,#31776,#31777,#31778,#31779),
 .UNSPECIFIED.,.F.,.F.,(4,1,4),(13.8759337553363,14.8089481060366,15.7079632679489),
 .UNSPECIFIED.);
#2167=B_SPLINE_CURVE_WITH_KNOTS('',3,(#31781,#31782,#31783,#31784,#31785,
#31786,#31787,#31788,#31789,#31790,#31791),.UNSPECIFIED.,.F.,.F.,(4,1,1,
1,1,1,1,1,4),(15.7079632679489,15.7922678539462,16.7755876018558,17.7589073497654,
18.742227097675,19.7255468455846,20.7088665934942,21.6921863414038,21.9911485751285),
 .UNSPECIFIED.);
#2168=B_SPLINE_CURVE_WITH_KNOTS('',3,(#31792,#31793,#31794,#31795,#31796,
#31797,#31798,#31799,#31800,#31801),.UNSPECIFIED.,.F.,.F.,(4,1,1,1,1,1,
1,4),(15.7079632679489,16.3650396227911,17.3483593707007,18.3316791186103,
19.3149988665199,20.2983186144295,21.2816383623391,21.9911485751285),
 .UNSPECIFIED.);
#2169=B_SPLINE_CURVE_WITH_KNOTS('',3,(#31950,#31951,#31952,#31953,#31954,
#31955,#31956,#31957,#31958,#31959,#31960,#31961,#31962,#31963,#31964,#31965,
#31966,#31967,#31968,#31969,#31970,#31971,#31972,#31973,#31974,#31975,#31976,
#31977,#31978,#31979,#31980,#31981,#31982,#31983,#31984,#31985,#31986,#31987,
#31988,#31989,#31990,#31991,#31992,#31993,#31994,#31995,#31996,#31997,#31998,
#31999,#32000,#32001,#32002,#32003,#32004,#32005,#32006,#32007,#32008,#32009,
#32010,#32011,#32012,#32013,#32014,#32015,#32016,#32017,#32018,#32019,#32020,
#32021,#32022,#32023,#32024,#32025,#32026,#32027,#32028,#32029,#32030,#32031,
#32032,#32033,#32034,#32035,#32036,#32037),.UNSPECIFIED.,.F.,.F.,(4,3,3,
3,3,3,3,3,3,3,3,3,3,3,3,3,3,3,3,3,3,3,3,3,3,3,3,3,3,4),(0.,0.0297382846428454,
0.0601255889259488,0.0890332382811597,0.114327431466969,0.120650702355347,
0.150403564921709,0.179988720829457,0.207838236564002,0.229395399392172,
0.23393415783729,0.262660470802463,0.291386783767636,0.320322059900051,
0.335078154046361,0.340193241308639,0.344573678198122,0.372678327643481,
0.400795960862634,0.428486852199556,0.439053852931727,0.445278633015735,
0.450309834423539,0.477267903159324,0.497055818929743,0.50468887016549,
0.511949053885254,0.537905662994819,0.556419566241001,0.569248610399422),
 .UNSPECIFIED.);
#2170=B_SPLINE_CURVE_WITH_KNOTS('',3,(#32038,#32039,#32040,#32041,#32042,
#32043,#32044,#32045,#32046,#32047,#32048,#32049,#32050,#32051,#32052,#32053,
#32054,#32055,#32056,#32057,#32058,#32059,#32060,#32061,#32062,#32063,#32064,
#32065,#32066,#32067,#32068,#32069,#32070,#32071,#32072,#32073,#32074,#32075,
#32076,#32077,#32078,#32079,#32080,#32081,#32082,#32083,#32084,#32085,#32086,
#32087,#32088,#32089,#32090,#32091,#32092,#32093,#32094,#32095,#32096,#32097,
#32098,#32099,#32100,#32101,#32102,#32103,#32104,#32105,#32106,#32107,#32108,
#32109,#32110,#32111,#32112,#32113,#32114,#32115,#32116,#32117,#32118,#32119,
#32120,#32121,#32122,#32123,#32124,#32125,#32126,#32127,#32128,#32129,#32130,
#32131),.UNSPECIFIED.,.F.,.F.,(4,3,3,3,3,3,3,3,3,3,3,3,3,3,3,3,3,3,3,3,
3,3,3,3,3,3,3,3,3,3,3,4),(0.,0.0253795104813928,0.0514287956022284,0.0778538073776754,
0.0899945430700518,0.0969018068642677,0.102642146791298,0.129947872947979,
0.157699027910297,0.183981493384174,0.195665040532001,0.201809460807294,
0.206412496951858,0.235040986639171,0.262828889805804,0.290686253909393,
0.306981212992593,0.31132393091396,0.315703998135388,0.34516669827354,0.374337762706802,
0.403793893800065,0.41497713906407,0.422789593408606,0.427299404513114,
0.458325953194986,0.48159586470639,0.493906250475823,0.500072154367986,
0.530578895950629,0.551405599240602,0.566847306048089),.UNSPECIFIED.);
#2171=B_SPLINE_CURVE_WITH_KNOTS('',3,(#32132,#32133,#32134,#32135,#32136,
#32137,#32138,#32139,#32140,#32141,#32142,#32143,#32144,#32145,#32146,#32147,
#32148,#32149,#32150,#32151,#32152,#32153,#32154,#32155,#32156),
 .UNSPECIFIED.,.F.,.F.,(4,3,3,3,3,3,3,3,4),(-10.1321597128207,-9.833197479096,
-8.8498777311864,-7.8665579832768,-6.8832382353672,-5.8999184874576,-4.916598739548,
-3.9332789916384,-3.84897440564114),.UNSPECIFIED.);
#2172=B_SPLINE_CURVE_WITH_KNOTS('',3,(#32305,#32306,#32307,#32308,#32309,
#32310,#32311,#32312,#32313,#32314,#32315,#32316,#32317,#32318,#32319,#32320,
#32321,#32322,#32323,#32324,#32325,#32326,#32327,#32328,#32329,#32330,#32331,
#32332,#32333,#32334,#32335,#32336,#32337,#32338,#32339,#32340,#32341,#32342,
#32343,#32344,#32345,#32346,#32347,#32348,#32349,#32350,#32351,#32352,#32353,
#32354,#32355,#32356,#32357,#32358,#32359,#32360,#32361,#32362,#32363,#32364,
#32365,#32366,#32367,#32368,#32369,#32370,#32371,#32372,#32373,#32374,#32375,
#32376,#32377,#32378,#32379,#32380,#32381,#32382,#32383,#32384,#32385,#32386,
#32387,#32388,#32389,#32390,#32391,#32392,#32393,#32394,#32395,#32396,#32397,
#32398),.UNSPECIFIED.,.F.,.F.,(4,3,3,3,3,3,3,3,3,3,3,3,3,3,3,3,3,3,3,3,
3,3,3,3,3,3,3,3,3,3,3,4),(0.,0.0253795895352918,0.0514289454719094,0.0778539385136474,
0.0899945864079409,0.0969018005134045,0.102642148135923,0.129947928392544,
0.157699108353734,0.183981553716754,0.195665088727664,0.201809360898104,
0.206412522774552,0.235041003890312,0.262828889805813,0.290686211240011,
0.306981172990049,0.311324022663455,0.315704013189775,0.345166711446132,
0.374337752779982,0.403793879145986,0.414977105191051,0.422789478907973,
0.427299173709167,0.458325780092032,0.481595734879181,0.493906100937864,
0.500072114794957,0.530578856744846,0.551405599240626,0.566847306048098),
 .UNSPECIFIED.);
#2173=B_SPLINE_CURVE_WITH_KNOTS('',3,(#32399,#32400,#32401,#32402,#32403,
#32404,#32405,#32406,#32407,#32408,#32409,#32410,#32411,#32412,#32413,#32414,
#32415,#32416,#32417,#32418,#32419,#32420,#32421,#32422,#32423),
 .UNSPECIFIED.,.F.,.F.,(4,3,3,3,3,3,3,3,4),(7.59274844815668,7.8665579832768,
8.84987773118639,9.833197479096,10.8165172270056,11.7998369749152,12.7831567228248,
13.7664764707344,13.8759337553363),.UNSPECIFIED.);
#2174=B_SPLINE_CURVE_WITH_KNOTS('',3,(#32424,#32425,#32426,#32427,#32428,
#32429,#32430,#32431,#32432,#32433,#32434,#32435,#32436,#32437,#32438,#32439,
#32440,#32441,#32442,#32443,#32444,#32445,#32446,#32447,#32448,#32449,#32450,
#32451,#32452,#32453,#32454,#32455,#32456,#32457,#32458,#32459,#32460,#32461,
#32462,#32463,#32464,#32465,#32466,#32467,#32468,#32469,#32470,#32471,#32472,
#32473,#32474,#32475,#32476,#32477,#32478,#32479,#32480,#32481,#32482,#32483,
#32484,#32485,#32486,#32487,#32488,#32489,#32490,#32491,#32492,#32493,#32494,
#32495,#32496,#32497,#32498,#32499,#32500,#32501,#32502,#32503,#32504,#32505,
#32506,#32507,#32508,#32509,#32510,#32511),.UNSPECIFIED.,.F.,.F.,(4,3,3,
3,3,3,3,3,3,3,3,3,3,3,3,3,3,3,3,3,3,3,3,3,3,3,3,3,3,4),(0.,0.0297383502225738,
0.0601256857797807,0.0890333230282637,0.114327505620686,0.120650688809437,
0.150403550371837,0.179988686667598,0.207838210942609,0.229395337968592,
0.23393415684471,0.262660470306177,0.291386783767645,0.32032206170552,0.335078155738989,
0.340193228824031,0.344573672707814,0.372678323504497,0.400795954000531,
0.428486824889168,0.439053762328703,0.445278745781163,0.450309838937034,
0.477267882086698,0.497055803125278,0.504688833353528,0.511949049757023,
0.537905617573998,0.556419566241016,0.569248610399434),.UNSPECIFIED.);
#2693=LINE('',#31458,#3239);
#2694=LINE('',#31479,#3240);
#2695=LINE('',#31530,#3241);
#2696=LINE('',#31581,#3242);
#2697=LINE('',#31629,#3243);
#2698=LINE('',#31668,#3244);
#2699=LINE('',#31692,#3245);
#2700=LINE('',#31716,#3246);
#2701=LINE('',#31741,#3247);
#2702=LINE('',#31766,#3248);
#2703=LINE('',#32515,#3249);
#2704=LINE('',#32517,#3250);
#2705=LINE('',#32519,#3251);
#2706=LINE('',#32521,#3252);
#2707=LINE('',#32523,#3253);
#2708=LINE('',#32524,#3254);
#2709=LINE('',#32529,#3255);
#2710=LINE('',#32530,#3256);
#2711=LINE('',#32531,#3257);
#2712=LINE('',#32534,#3258);
#2713=LINE('',#32535,#3259);
#2714=LINE('',#32538,#3260);
#2715=LINE('',#32539,#3261);
#2716=LINE('',#32542,#3262);
#2717=LINE('',#32543,#3263);
#2718=LINE('',#32546,#3264);
#2719=LINE('',#32547,#3265);
#2720=LINE('',#32549,#3266);
#3239=VECTOR('',#11201,3.);
#3240=VECTOR('',#11206,3.);
#3241=VECTOR('',#11209,3.);
#3242=VECTOR('',#11212,3.);
#3243=VECTOR('',#11215,3.);
#3244=VECTOR('',#11220,3.0735);
#3245=VECTOR('',#11225,3.0735);
#3246=VECTOR('',#11228,3.0735);
#3247=VECTOR('',#11231,3.0735);
#3248=VECTOR('',#11234,3.0735);
#3249=VECTOR('',#11241,10.);
#3250=VECTOR('',#11242,10.);
#3251=VECTOR('',#11243,10.);
#3252=VECTOR('',#11244,10.);
#3253=VECTOR('',#11245,10.);
#3254=VECTOR('',#11246,10.);
#3255=VECTOR('',#11251,10.);
#3256=VECTOR('',#11252,10.);
#3257=VECTOR('',#11253,10.);
#3258=VECTOR('',#11256,10.);
#3259=VECTOR('',#11257,10.);
#3260=VECTOR('',#11260,10.);
#3261=VECTOR('',#11261,10.);
#3262=VECTOR('',#11264,10.);
#3263=VECTOR('',#11265,10.);
#3264=VECTOR('',#11268,10.);
#3265=VECTOR('',#11269,10.);
#3266=VECTOR('',#11272,10.);
#4067=VERTEX_POINT('',#31456);
#4068=VERTEX_POINT('',#31457);
#4069=VERTEX_POINT('',#31459);
#4070=VERTEX_POINT('',#31464);
#4071=VERTEX_POINT('',#31477);
#4072=VERTEX_POINT('',#31478);
#4073=VERTEX_POINT('',#31528);
#4074=VERTEX_POINT('',#31529);
#4075=VERTEX_POINT('',#31579);
#4076=VERTEX_POINT('',#31580);
#4077=VERTEX_POINT('',#31627);
#4078=VERTEX_POINT('',#31628);
#4079=VERTEX_POINT('',#31630);
#4080=VERTEX_POINT('',#31644);
#4081=VERTEX_POINT('',#31666);
#4082=VERTEX_POINT('',#31667);
#4083=VERTEX_POINT('',#31669);
#4084=VERTEX_POINT('',#31678);
#4085=VERTEX_POINT('',#31690);
#4086=VERTEX_POINT('',#31691);
#4087=VERTEX_POINT('',#31714);
#4088=VERTEX_POINT('',#31715);
#4089=VERTEX_POINT('',#31739);
#4090=VERTEX_POINT('',#31740);
#4091=VERTEX_POINT('',#31764);
#4092=VERTEX_POINT('',#31765);
#4093=VERTEX_POINT('',#31767);
#4094=VERTEX_POINT('',#31773);
#4095=VERTEX_POINT('',#32513);
#4096=VERTEX_POINT('',#32514);
#4097=VERTEX_POINT('',#32516);
#4098=VERTEX_POINT('',#32518);
#4099=VERTEX_POINT('',#32520);
#4100=VERTEX_POINT('',#32522);
#4101=VERTEX_POINT('',#32527);
#4102=VERTEX_POINT('',#32528);
#4103=VERTEX_POINT('',#32533);
#4104=VERTEX_POINT('',#32537);
#4105=VERTEX_POINT('',#32541);
#4106=VERTEX_POINT('',#32545);
#5307=EDGE_CURVE('',#4067,#4068,#2693,.T.);
#5308=EDGE_CURVE('',#4068,#4069,#2147,.T.);
#5309=EDGE_CURVE('',#4070,#4069,#1581,.F.);
#5310=EDGE_CURVE('',#4070,#4067,#2148,.T.);
#5311=EDGE_CURVE('',#4071,#4072,#2694,.T.);
#5312=EDGE_CURVE('',#4072,#4068,#2149,.T.);
#5313=EDGE_CURVE('',#4067,#4071,#2150,.T.);
#5314=EDGE_CURVE('',#4073,#4074,#2695,.T.);
#5315=EDGE_CURVE('',#4074,#4072,#2151,.T.);
#5316=EDGE_CURVE('',#4071,#4073,#2152,.T.);
#5317=EDGE_CURVE('',#4075,#4076,#2696,.T.);
#5318=EDGE_CURVE('',#4076,#4074,#2153,.T.);
#5319=EDGE_CURVE('',#4073,#4075,#2154,.T.);
#5320=EDGE_CURVE('',#4077,#4078,#2697,.T.);
#5321=EDGE_CURVE('',#4077,#4079,#2155,.T.);
#5322=EDGE_CURVE('',#4080,#4079,#1582,.T.);
#5323=EDGE_CURVE('',#4080,#4078,#2156,.T.);
#5324=EDGE_CURVE('',#4081,#4082,#2698,.T.);
#5325=EDGE_CURVE('',#4082,#4083,#2157,.T.);
#5326=EDGE_CURVE('',#4084,#4083,#1583,.T.);
#5327=EDGE_CURVE('',#4081,#4084,#2158,.T.);
#5328=EDGE_CURVE('',#4085,#4086,#2699,.T.);
#5329=EDGE_CURVE('',#4086,#4082,#2159,.T.);
#5330=EDGE_CURVE('',#4085,#4081,#2160,.T.);
#5331=EDGE_CURVE('',#4087,#4088,#2700,.T.);
#5332=EDGE_CURVE('',#4088,#4086,#2161,.T.);
#5333=EDGE_CURVE('',#4087,#4085,#2162,.T.);
#5334=EDGE_CURVE('',#4089,#4090,#2701,.T.);
#5335=EDGE_CURVE('',#4090,#4088,#2163,.T.);
#5336=EDGE_CURVE('',#4089,#4087,#2164,.T.);
#5337=EDGE_CURVE('',#4091,#4092,#2702,.T.);
#5338=EDGE_CURVE('',#4093,#4091,#2165,.T.);
#5339=EDGE_CURVE('',#4094,#4093,#1584,.T.);
#5340=EDGE_CURVE('',#4094,#4092,#2166,.T.);
#5341=EDGE_CURVE('',#4092,#4090,#2167,.T.);
#5342=EDGE_CURVE('',#4091,#4089,#2168,.T.);
#5343=EDGE_CURVE('',#4083,#4070,#2169,.T.);
#5344=EDGE_CURVE('',#4079,#4094,#2170,.T.);
#5345=EDGE_CURVE('',#4075,#4077,#2171,.T.);
#5346=EDGE_CURVE('',#4069,#4084,#2172,.T.);
#5347=EDGE_CURVE('',#4078,#4076,#2173,.T.);
#5348=EDGE_CURVE('',#4093,#4080,#2174,.T.);
#5349=EDGE_CURVE('',#4095,#4096,#2703,.T.);
#5350=EDGE_CURVE('',#4096,#4097,#2704,.T.);
#5351=EDGE_CURVE('',#4097,#4098,#2705,.T.);
#5352=EDGE_CURVE('',#4098,#4099,#2706,.T.);
#5353=EDGE_CURVE('',#4099,#4100,#2707,.T.);
#5354=EDGE_CURVE('',#4100,#4095,#2708,.T.);
#5355=EDGE_CURVE('',#4101,#4102,#2709,.T.);
#5356=EDGE_CURVE('',#4102,#4095,#2710,.T.);
#5357=EDGE_CURVE('',#4101,#4100,#2711,.T.);
#5358=EDGE_CURVE('',#4103,#4101,#2712,.T.);
#5359=EDGE_CURVE('',#4103,#4099,#2713,.T.);
#5360=EDGE_CURVE('',#4104,#4103,#2714,.T.);
#5361=EDGE_CURVE('',#4104,#4098,#2715,.T.);
#5362=EDGE_CURVE('',#4105,#4104,#2716,.T.);
#5363=EDGE_CURVE('',#4105,#4097,#2717,.T.);
#5364=EDGE_CURVE('',#4106,#4105,#2718,.T.);
#5365=EDGE_CURVE('',#4106,#4096,#2719,.T.);
#5366=EDGE_CURVE('',#4102,#4106,#2720,.T.);
#7767=ORIENTED_EDGE('',*,*,#5307,.T.);
#7768=ORIENTED_EDGE('',*,*,#5308,.T.);
#7769=ORIENTED_EDGE('',*,*,#5309,.F.);
#7770=ORIENTED_EDGE('',*,*,#5310,.T.);
#7771=ORIENTED_EDGE('',*,*,#5311,.T.);
#7772=ORIENTED_EDGE('',*,*,#5312,.T.);
#7773=ORIENTED_EDGE('',*,*,#5307,.F.);
#7774=ORIENTED_EDGE('',*,*,#5313,.T.);
#7775=ORIENTED_EDGE('',*,*,#5314,.T.);
#7776=ORIENTED_EDGE('',*,*,#5315,.T.);
#7777=ORIENTED_EDGE('',*,*,#5311,.F.);
#7778=ORIENTED_EDGE('',*,*,#5316,.T.);
#7779=ORIENTED_EDGE('',*,*,#5317,.T.);
#7780=ORIENTED_EDGE('',*,*,#5318,.T.);
#7781=ORIENTED_EDGE('',*,*,#5314,.F.);
#7782=ORIENTED_EDGE('',*,*,#5319,.T.);
#7783=ORIENTED_EDGE('',*,*,#5320,.F.);
#7784=ORIENTED_EDGE('',*,*,#5321,.T.);
#7785=ORIENTED_EDGE('',*,*,#5322,.F.);
#7786=ORIENTED_EDGE('',*,*,#5323,.T.);
#7787=ORIENTED_EDGE('',*,*,#5324,.T.);
#7788=ORIENTED_EDGE('',*,*,#5325,.T.);
#7789=ORIENTED_EDGE('',*,*,#5326,.F.);
#7790=ORIENTED_EDGE('',*,*,#5327,.F.);
#7791=ORIENTED_EDGE('',*,*,#5328,.T.);
#7792=ORIENTED_EDGE('',*,*,#5329,.T.);
#7793=ORIENTED_EDGE('',*,*,#5324,.F.);
#7794=ORIENTED_EDGE('',*,*,#5330,.F.);
#7795=ORIENTED_EDGE('',*,*,#5331,.T.);
#7796=ORIENTED_EDGE('',*,*,#5332,.T.);
#7797=ORIENTED_EDGE('',*,*,#5328,.F.);
#7798=ORIENTED_EDGE('',*,*,#5333,.F.);
#7799=ORIENTED_EDGE('',*,*,#5334,.T.);
#7800=ORIENTED_EDGE('',*,*,#5335,.T.);
#7801=ORIENTED_EDGE('',*,*,#5331,.F.);
#7802=ORIENTED_EDGE('',*,*,#5336,.F.);
#7803=ORIENTED_EDGE('',*,*,#5337,.F.);
#7804=ORIENTED_EDGE('',*,*,#5338,.F.);
#7805=ORIENTED_EDGE('',*,*,#5339,.F.);
#7806=ORIENTED_EDGE('',*,*,#5340,.T.);
#7807=ORIENTED_EDGE('',*,*,#5337,.T.);
#7808=ORIENTED_EDGE('',*,*,#5341,.T.);
#7809=ORIENTED_EDGE('',*,*,#5334,.F.);
#7810=ORIENTED_EDGE('',*,*,#5342,.F.);
#7811=ORIENTED_EDGE('',*,*,#5343,.F.);
#7812=ORIENTED_EDGE('',*,*,#5325,.F.);
#7813=ORIENTED_EDGE('',*,*,#5329,.F.);
#7814=ORIENTED_EDGE('',*,*,#5332,.F.);
#7815=ORIENTED_EDGE('',*,*,#5335,.F.);
#7816=ORIENTED_EDGE('',*,*,#5341,.F.);
#7817=ORIENTED_EDGE('',*,*,#5340,.F.);
#7818=ORIENTED_EDGE('',*,*,#5344,.F.);
#7819=ORIENTED_EDGE('',*,*,#5321,.F.);
#7820=ORIENTED_EDGE('',*,*,#5345,.F.);
#7821=ORIENTED_EDGE('',*,*,#5319,.F.);
#7822=ORIENTED_EDGE('',*,*,#5316,.F.);
#7823=ORIENTED_EDGE('',*,*,#5313,.F.);
#7824=ORIENTED_EDGE('',*,*,#5310,.F.);
#7825=ORIENTED_EDGE('',*,*,#5346,.F.);
#7826=ORIENTED_EDGE('',*,*,#5308,.F.);
#7827=ORIENTED_EDGE('',*,*,#5312,.F.);
#7828=ORIENTED_EDGE('',*,*,#5315,.F.);
#7829=ORIENTED_EDGE('',*,*,#5318,.F.);
#7830=ORIENTED_EDGE('',*,*,#5347,.F.);
#7831=ORIENTED_EDGE('',*,*,#5323,.F.);
#7832=ORIENTED_EDGE('',*,*,#5348,.F.);
#7833=ORIENTED_EDGE('',*,*,#5338,.T.);
#7834=ORIENTED_EDGE('',*,*,#5342,.T.);
#7835=ORIENTED_EDGE('',*,*,#5336,.T.);
#7836=ORIENTED_EDGE('',*,*,#5333,.T.);
#7837=ORIENTED_EDGE('',*,*,#5330,.T.);
#7838=ORIENTED_EDGE('',*,*,#5327,.T.);
#7839=ORIENTED_EDGE('',*,*,#5349,.T.);
#7840=ORIENTED_EDGE('',*,*,#5350,.T.);
#7841=ORIENTED_EDGE('',*,*,#5351,.T.);
#7842=ORIENTED_EDGE('',*,*,#5352,.T.);
#7843=ORIENTED_EDGE('',*,*,#5353,.T.);
#7844=ORIENTED_EDGE('',*,*,#5354,.T.);
#7845=ORIENTED_EDGE('',*,*,#5344,.T.);
#7846=ORIENTED_EDGE('',*,*,#5339,.T.);
#7847=ORIENTED_EDGE('',*,*,#5348,.T.);
#7848=ORIENTED_EDGE('',*,*,#5322,.T.);
#7849=ORIENTED_EDGE('',*,*,#5320,.T.);
#7850=ORIENTED_EDGE('',*,*,#5347,.T.);
#7851=ORIENTED_EDGE('',*,*,#5317,.F.);
#7852=ORIENTED_EDGE('',*,*,#5345,.T.);
#7853=ORIENTED_EDGE('',*,*,#5355,.T.);
#7854=ORIENTED_EDGE('',*,*,#5356,.T.);
#7855=ORIENTED_EDGE('',*,*,#5354,.F.);
#7856=ORIENTED_EDGE('',*,*,#5357,.F.);
#7857=ORIENTED_EDGE('',*,*,#5358,.T.);
#7858=ORIENTED_EDGE('',*,*,#5357,.T.);
#7859=ORIENTED_EDGE('',*,*,#5353,.F.);
#7860=ORIENTED_EDGE('',*,*,#5359,.F.);
#7861=ORIENTED_EDGE('',*,*,#5360,.T.);
#7862=ORIENTED_EDGE('',*,*,#5359,.T.);
#7863=ORIENTED_EDGE('',*,*,#5352,.F.);
#7864=ORIENTED_EDGE('',*,*,#5361,.F.);
#7865=ORIENTED_EDGE('',*,*,#5362,.T.);
#7866=ORIENTED_EDGE('',*,*,#5361,.T.);
#7867=ORIENTED_EDGE('',*,*,#5351,.F.);
#7868=ORIENTED_EDGE('',*,*,#5363,.F.);
#7869=ORIENTED_EDGE('',*,*,#5364,.T.);
#7870=ORIENTED_EDGE('',*,*,#5363,.T.);
#7871=ORIENTED_EDGE('',*,*,#5350,.F.);
#7872=ORIENTED_EDGE('',*,*,#5365,.F.);
#7873=ORIENTED_EDGE('',*,*,#5366,.T.);
#7874=ORIENTED_EDGE('',*,*,#5365,.T.);
#7875=ORIENTED_EDGE('',*,*,#5349,.F.);
#7876=ORIENTED_EDGE('',*,*,#5356,.F.);
#7877=ORIENTED_EDGE('',*,*,#5366,.F.);
#7878=ORIENTED_EDGE('',*,*,#5355,.F.);
#7879=ORIENTED_EDGE('',*,*,#5358,.F.);
#7880=ORIENTED_EDGE('',*,*,#5360,.F.);
#7881=ORIENTED_EDGE('',*,*,#5362,.F.);
#7882=ORIENTED_EDGE('',*,*,#5364,.F.);
#7883=ORIENTED_EDGE('',*,*,#5343,.T.);
#7884=ORIENTED_EDGE('',*,*,#5309,.T.);
#7885=ORIENTED_EDGE('',*,*,#5346,.T.);
#7886=ORIENTED_EDGE('',*,*,#5326,.T.);
#8188=CYLINDRICAL_SURFACE('',#9468,2.5175);
#8189=CYLINDRICAL_SURFACE('',#9470,2.5175);
#8190=CYLINDRICAL_SURFACE('',#9471,2.5175);
#8191=CYLINDRICAL_SURFACE('',#9472,2.5175);
#8192=CYLINDRICAL_SURFACE('',#9473,2.5175);
#8193=CYLINDRICAL_SURFACE('',#9475,3.0735);
#8194=CYLINDRICAL_SURFACE('',#9477,3.0735);
#8195=CYLINDRICAL_SURFACE('',#9478,3.0735);
#8196=CYLINDRICAL_SURFACE('',#9479,3.0735);
#8197=CYLINDRICAL_SURFACE('',#9480,3.0735);
#8198=CYLINDRICAL_SURFACE('',#9482,3.0735);
#8199=CYLINDRICAL_SURFACE('',#9484,2.5175);
#8653=ADVANCED_FACE('',(#905),#8188,.F.);
#8654=ADVANCED_FACE('',(#906),#8189,.F.);
#8655=ADVANCED_FACE('',(#907),#8190,.F.);
#8656=ADVANCED_FACE('',(#908),#8191,.F.);
#8657=ADVANCED_FACE('',(#909),#8192,.F.);
#8658=ADVANCED_FACE('',(#910),#8193,.F.);
#8659=ADVANCED_FACE('',(#911),#8194,.F.);
#8660=ADVANCED_FACE('',(#912),#8195,.F.);
#8661=ADVANCED_FACE('',(#913),#8196,.F.);
#8662=ADVANCED_FACE('',(#914),#8197,.F.);
#8663=ADVANCED_FACE('',(#915),#8198,.F.);
#8664=ADVANCED_FACE('',(#916),#309,.F.);
#8665=ADVANCED_FACE('',(#917),#310,.F.);
#8666=ADVANCED_FACE('',(#918,#291),#444,.T.);
#8667=ADVANCED_FACE('',(#919),#8199,.F.);
#8668=ADVANCED_FACE('',(#920),#445,.T.);
#8669=ADVANCED_FACE('',(#921),#446,.T.);
#8670=ADVANCED_FACE('',(#922),#447,.T.);
#8671=ADVANCED_FACE('',(#923),#448,.T.);
#8672=ADVANCED_FACE('',(#924),#449,.T.);
#8673=ADVANCED_FACE('',(#925),#450,.T.);
#8674=ADVANCED_FACE('',(#926,#292),#451,.F.);
#8692=CLOSED_SHELL('',(#8653,#8654,#8655,#8656,#8657,#8658,#8659,#8660,
#8661,#8662,#8663,#8664,#8665,#8666,#8667,#8668,#8669,#8670,#8671,#8672,
#8673,#8674));
#9467=AXIS2_PLACEMENT_3D('',#31454,#11197,#11198);
#9468=AXIS2_PLACEMENT_3D('',#31455,#11199,#11200);
#9469=AXIS2_PLACEMENT_3D('',#31465,#11202,#11203);
#9470=AXIS2_PLACEMENT_3D('',#31476,#11204,#11205);
#9471=AXIS2_PLACEMENT_3D('',#31527,#11207,#11208);
#9472=AXIS2_PLACEMENT_3D('',#31578,#11210,#11211);
#9473=AXIS2_PLACEMENT_3D('',#31626,#11213,#11214);
#9474=AXIS2_PLACEMENT_3D('',#31645,#11216,#11217);
#9475=AXIS2_PLACEMENT_3D('',#31665,#11218,#11219);
#9476=AXIS2_PLACEMENT_3D('',#31679,#11221,#11222);
#9477=AXIS2_PLACEMENT_3D('',#31689,#11223,#11224);
#9478=AXIS2_PLACEMENT_3D('',#31713,#11226,#11227);
#9479=AXIS2_PLACEMENT_3D('',#31738,#11229,#11230);
#9480=AXIS2_PLACEMENT_3D('',#31763,#11232,#11233);
#9481=AXIS2_PLACEMENT_3D('',#31774,#11235,#11236);
#9482=AXIS2_PLACEMENT_3D('',#31780,#11237,#11238);
#9483=AXIS2_PLACEMENT_3D('',#32512,#11239,#11240);
#9484=AXIS2_PLACEMENT_3D('',#32525,#11247,#11248);
#9485=AXIS2_PLACEMENT_3D('',#32526,#11249,#11250);
#9486=AXIS2_PLACEMENT_3D('',#32532,#11254,#11255);
#9487=AXIS2_PLACEMENT_3D('',#32536,#11258,#11259);
#9488=AXIS2_PLACEMENT_3D('',#32540,#11262,#11263);
#9489=AXIS2_PLACEMENT_3D('',#32544,#11266,#11267);
#9490=AXIS2_PLACEMENT_3D('',#32548,#11270,#11271);
#9491=AXIS2_PLACEMENT_3D('',#32550,#11273,#11274);
#11197=DIRECTION('axis',(0.,0.,1.));
#11198=DIRECTION('refdir',(1.,0.,0.));
#11199=DIRECTION('center_axis',(0.,0.,-1.));
#11200=DIRECTION('ref_axis',(-0.346824478021586,0.937930051467088,0.));
#11201=DIRECTION('',(0.,0.,-1.));
#11202=DIRECTION('center_axis',(0.,0.,-1.));
#11203=DIRECTION('ref_axis',(1.,0.,0.));
#11204=DIRECTION('center_axis',(0.,0.,-1.));
#11205=DIRECTION('ref_axis',(1.,0.,0.));
#11206=DIRECTION('',(0.,0.,-1.));
#11207=DIRECTION('center_axis',(0.,0.,-1.));
#11208=DIRECTION('ref_axis',(1.,0.,0.));
#11209=DIRECTION('',(0.,0.,-1.));
#11210=DIRECTION('center_axis',(0.,0.,-1.));
#11211=DIRECTION('ref_axis',(1.,0.,0.));
#11212=DIRECTION('',(0.,0.,-1.));
#11213=DIRECTION('center_axis',(0.,0.,-1.));
#11214=DIRECTION('ref_axis',(0.937996590358642,-0.346644481386278,0.));
#11215=DIRECTION('',(0.,0.,-1.));
#11216=DIRECTION('center_axis',(0.,0.,-1.));
#11217=DIRECTION('ref_axis',(1.,0.,0.));
#11218=DIRECTION('center_axis',(0.,0.,-1.));
#11219=DIRECTION('ref_axis',(0.7932173491397,0.608938615152452,0.));
#11220=DIRECTION('',(1.22464679914735E-16,-9.27389451825078E-31,-1.));
#11221=DIRECTION('center_axis',(0.,0.,1.));
#11222=DIRECTION('ref_axis',(1.,-7.45024487577726E-15,0.));
#11223=DIRECTION('center_axis',(0.,0.,-1.));
#11224=DIRECTION('ref_axis',(1.,-7.45024487577726E-15,0.));
#11225=DIRECTION('',(1.22464679914735E-16,-9.27389451825078E-31,-1.));
#11226=DIRECTION('center_axis',(0.,0.,-1.));
#11227=DIRECTION('ref_axis',(1.,-7.45024487577726E-15,0.));
#11228=DIRECTION('',(1.22464679914735E-16,-9.27389451825078E-31,-1.));
#11229=DIRECTION('center_axis',(0.,0.,-1.));
#11230=DIRECTION('ref_axis',(1.,-7.45024487577726E-15,0.));
#11231=DIRECTION('',(1.22464679914735E-16,-9.27389451825078E-31,-1.));
#11232=DIRECTION('center_axis',(0.,0.,-1.));
#11233=DIRECTION('ref_axis',(-0.609064819364946,-0.793120448489348,0.));
#11234=DIRECTION('',(1.22464679914735E-16,-9.27389451825078E-31,-1.));
#11235=DIRECTION('center_axis',(0.,0.,-1.));
#11236=DIRECTION('ref_axis',(1.,-7.45024487577726E-15,0.));
#11237=DIRECTION('center_axis',(0.,0.,-1.));
#11238=DIRECTION('ref_axis',(1.,-7.45024487577726E-15,0.));
#11239=DIRECTION('center_axis',(0.,0.,1.));
#11240=DIRECTION('ref_axis',(1.,0.,0.));
#11241=DIRECTION('',(0.5,0.866025403784439,0.));
#11242=DIRECTION('',(-0.5,0.866025403784439,0.));
#11243=DIRECTION('',(-1.,1.92296268638356E-16,0.));
#11244=DIRECTION('',(-0.5,-0.866025403784439,0.));
#11245=DIRECTION('',(0.5,-0.866025403784439,0.));
#11246=DIRECTION('',(1.,-1.92296268638356E-16,0.));
#11247=DIRECTION('center_axis',(0.,0.,-1.));
#11248=DIRECTION('ref_axis',(1.,0.,0.));
#11249=DIRECTION('center_axis',(-1.92296268638356E-16,-1.,0.));
#11250=DIRECTION('ref_axis',(1.,-1.92296268638356E-16,0.));
#11251=DIRECTION('',(1.,-1.92296268638356E-16,0.));
#11252=DIRECTION('',(0.,0.,1.));
#11253=DIRECTION('',(0.,0.,1.));
#11254=DIRECTION('center_axis',(-0.866025403784439,-0.5,0.));
#11255=DIRECTION('ref_axis',(0.5,-0.866025403784439,0.));
#11256=DIRECTION('',(0.5,-0.866025403784439,0.));
#11257=DIRECTION('',(0.,0.,1.));
#11258=DIRECTION('center_axis',(-0.866025403784439,0.5,0.));
#11259=DIRECTION('ref_axis',(-0.5,-0.866025403784438,0.));
#11260=DIRECTION('',(-0.5,-0.866025403784439,0.));
#11261=DIRECTION('',(0.,0.,1.));
#11262=DIRECTION('center_axis',(1.92296268638356E-16,1.,0.));
#11263=DIRECTION('ref_axis',(-1.,1.92296268638356E-16,0.));
#11264=DIRECTION('',(-1.,1.92296268638356E-16,0.));
#11265=DIRECTION('',(0.,0.,1.));
#11266=DIRECTION('center_axis',(0.866025403784439,0.5,0.));
#11267=DIRECTION('ref_axis',(-0.5,0.866025403784439,0.));
#11268=DIRECTION('',(-0.5,0.866025403784439,0.));
#11269=DIRECTION('',(0.,0.,1.));
#11270=DIRECTION('center_axis',(0.866025403784439,-0.5,0.));
#11271=DIRECTION('ref_axis',(0.5,0.866025403784439,0.));
#11272=DIRECTION('',(0.5,0.866025403784439,0.));
#11273=DIRECTION('center_axis',(0.,0.,1.));
#11274=DIRECTION('ref_axis',(1.,0.,0.));
#31454=CARTESIAN_POINT('',(0.,0.,0.));
#31455=CARTESIAN_POINT('Origin',(0.,0.,2.5));
#31456=CARTESIAN_POINT('',(-2.513631052301,-0.000262637959241863,0.387416697508025));
#31457=CARTESIAN_POINT('',(-2.5161395146468,-0.00304292125110089,0.112583302491978));
#31458=CARTESIAN_POINT('',(-2.5175,3.08304831685346E-16,2.5));
#31459=CARTESIAN_POINT('',(-1.91346599666505,1.63598720337496,0.));
#31460=CARTESIAN_POINT('Ctrl Pts',(-2.5161395146468,-0.00304292125110089,
0.112583302491978));
#31461=CARTESIAN_POINT('Ctrl Pts',(-2.51095752260429,0.58940711336228,0.0750555349946524));
#31462=CARTESIAN_POINT('Ctrl Pts',(-2.29922182808405,1.18480356030441,0.0375277674973267));
#31463=CARTESIAN_POINT('Ctrl Pts',(-1.91346599666507,1.63598720337494,7.63278329429795E-16));
#31464=CARTESIAN_POINT('',(1.9169334902101,1.63821054532066,9.12403139361656E-16));
#31465=CARTESIAN_POINT('Origin',(0.,0.,0.));
#31466=CARTESIAN_POINT('Ctrl Pts',(1.91694983752521,1.63822102714878,3.46944695195361E-16));
#31467=CARTESIAN_POINT('Ctrl Pts',(1.40805405000164,2.22926133126499,0.0494979486298783));
#31468=CARTESIAN_POINT('Ctrl Pts',(0.602342674674628,2.56946547367296,0.0989958972597568));
#31469=CARTESIAN_POINT('Ctrl Pts',(-0.175477465753492,2.51505986110806,
0.148493845889635));
#31470=CARTESIAN_POINT('Ctrl Pts',(-0.995235386765838,2.4577208574882,0.200660578729532));
#31471=CARTESIAN_POINT('Ctrl Pts',(-1.7840133645033,1.96207254741093,0.252827311569428));
#31472=CARTESIAN_POINT('Ctrl Pts',(-2.1906858971079,1.24828644590423,0.304994044409325));
#31473=CARTESIAN_POINT('Ctrl Pts',(-2.40486472497323,0.872362678473624,
0.332468262108891));
#31474=CARTESIAN_POINT('Ctrl Pts',(-2.51305801188577,0.435933487418771,
0.359942479808458));
#31475=CARTESIAN_POINT('Ctrl Pts',(-2.513631052301,-0.000262637959241863,
0.387416697508025));
#31476=CARTESIAN_POINT('Origin',(0.,0.,2.5));
#31477=CARTESIAN_POINT('',(-2.52068696412108,-0.00113551940461809,1.38741669750803));
#31478=CARTESIAN_POINT('',(-2.52025742113573,0.00144393706437333,1.11258330249198));
#31479=CARTESIAN_POINT('',(-2.5175,3.08304831685346E-16,2.5));
#31480=CARTESIAN_POINT('Ctrl Pts',(-2.52025742113573,0.00144393706437333,
1.11258330249198));
#31481=CARTESIAN_POINT('Ctrl Pts',(-2.52087167159714,0.0912295143008042,
1.10688933154059));
#31482=CARTESIAN_POINT('Ctrl Pts',(-2.51647663371758,0.180953836073687,
1.10119536058921));
#31483=CARTESIAN_POINT('Ctrl Pts',(-2.50686975205229,0.270115985573038,
1.09550138963782));
#31484=CARTESIAN_POINT('Ctrl Pts',(-2.41885391327537,1.08699722224894,1.04333465679793));
#31485=CARTESIAN_POINT('Ctrl Pts',(-1.89336817952545,1.85669104203942,0.991167923958032));
#31486=CARTESIAN_POINT('Ctrl Pts',(-1.16464801024837,2.23624073783096,0.939001191118135));
#31487=CARTESIAN_POINT('Ctrl Pts',(-0.435927840971309,2.6157904336225,0.886834458278239));
#31488=CARTESIAN_POINT('Ctrl Pts',(0.496026763832904,2.60519600541511,0.834667725438342));
#31489=CARTESIAN_POINT('Ctrl Pts',(1.21582156787348,2.20894038730756,0.782500992598446));
#31490=CARTESIAN_POINT('Ctrl Pts',(1.93561637191406,1.81268476920001,0.73033425975855));
#31491=CARTESIAN_POINT('Ctrl Pts',(2.443251375191,1.03076796119231,0.678167526918654));
#31492=CARTESIAN_POINT('Ctrl Pts',(2.51242958730335,0.212179626056957,0.626000794078758));
#31493=CARTESIAN_POINT('Ctrl Pts',(2.58160779941571,-0.606408709078402,
0.573834061238861));
#31494=CARTESIAN_POINT('Ctrl Pts',(2.21232922036347,-1.46166857134141,0.521667328398964));
#31495=CARTESIAN_POINT('Ctrl Pts',(1.56924485086725,-1.97326693907424,0.469500595559067));
#31496=CARTESIAN_POINT('Ctrl Pts',(0.926160481371042,-2.48486530680706,
0.417333862719171));
#31497=CARTESIAN_POINT('Ctrl Pts',(0.00927032143085621,-2.65280218000971,
0.365167129879276));
#31498=CARTESIAN_POINT('Ctrl Pts',(-0.772843960767751,-2.40046341131198,
0.31300039703938));
#31499=CARTESIAN_POINT('Ctrl Pts',(-1.55495824296637,-2.14812464261425,
0.260833664199484));
#31500=CARTESIAN_POINT('Ctrl Pts',(-2.2022966474234,-1.47551023201612,0.208666931359586));
#31501=CARTESIAN_POINT('Ctrl Pts',(-2.42598179621524,-0.686278012308338,
0.15650019851969));
#31502=CARTESIAN_POINT('Ctrl Pts',(-2.48875205155903,-0.464804623376722,
0.141861233177119));
#31503=CARTESIAN_POINT('Ctrl Pts',(-2.51816092457802,-0.234147943006738,
0.127222267834549));
#31504=CARTESIAN_POINT('Ctrl Pts',(-2.5161395146468,-0.00304292125110089,
0.112583302491978));
#31505=CARTESIAN_POINT('Ctrl Pts',(-2.513631052301,-0.000262637959241863,
0.387416697508025));
#31506=CARTESIAN_POINT('Ctrl Pts',(-2.51414607366698,-0.392294889717208,
0.412109212648355));
#31507=CARTESIAN_POINT('Ctrl Pts',(-2.42773023634316,-0.784138881365407,
0.436801727788684));
#31508=CARTESIAN_POINT('Ctrl Pts',(-2.25319678957557,-1.13170015918752,
0.461494242929014));
#31509=CARTESIAN_POINT('Ctrl Pts',(-1.88446806196691,-1.86597676983647,
0.51366097576891));
#31510=CARTESIAN_POINT('Ctrl Pts',(-1.12244351927786,-2.40260609819826,
0.565827708608806));
#31511=CARTESIAN_POINT('Ctrl Pts',(-0.306910970062746,-2.50259594233506,
0.617994441448702));
#31512=CARTESIAN_POINT('Ctrl Pts',(0.508621579152378,-2.60258578647186,
0.670161174288599));
#31513=CARTESIAN_POINT('Ctrl Pts',(1.37766213489358,-2.26593614638367,0.722327907128496));
#31514=CARTESIAN_POINT('Ctrl Pts',(1.91291169988306,-1.64259837236496,0.774494639968393));
#31515=CARTESIAN_POINT('Ctrl Pts',(2.44816126487255,-1.01926059834626,0.826661372808289));
#31516=CARTESIAN_POINT('Ctrl Pts',(2.64961983911033,-0.109234690397042,
0.878828105648185));
#31517=CARTESIAN_POINT('Ctrl Pts',(2.42745590365758,0.681791395088116,0.930994838488081));
#31518=CARTESIAN_POINT('Ctrl Pts',(2.20529196820482,1.47281748057328,0.983161571327977));
#31519=CARTESIAN_POINT('Ctrl Pts',(1.55950552306154,2.14484374359438,1.03532830416787));
#31520=CARTESIAN_POINT('Ctrl Pts',(0.777965481968195,2.39835160459691,1.08749503700777));
#31521=CARTESIAN_POINT('Ctrl Pts',(-0.00357455912515306,2.65185946559944,
1.13966176984767));
#31522=CARTESIAN_POINT('Ctrl Pts',(-0.920868196168557,2.48684892458339,
1.19182850268756));
#31523=CARTESIAN_POINT('Ctrl Pts',(-1.56505239016155,1.97685639415684,1.24399523552746));
#31524=CARTESIAN_POINT('Ctrl Pts',(-2.15540204953033,1.50948398821232,1.29180238952098));
#31525=CARTESIAN_POINT('Ctrl Pts',(-2.51638244467258,0.752380607759215,
1.3396095435145));
#31526=CARTESIAN_POINT('Ctrl Pts',(-2.52068696412108,-0.00113551940461809,
1.38741669750803));
#31527=CARTESIAN_POINT('Origin',(0.,0.,2.5));
#31528=CARTESIAN_POINT('',(-2.51584480336699,0.00196506899055149,2.38741669750802));
#31529=CARTESIAN_POINT('',(-2.51363229639634,1.41266446666228E-5,2.11258330249198));
#31530=CARTESIAN_POINT('',(-2.5175,3.08304831685346E-16,2.5));
#31531=CARTESIAN_POINT('Ctrl Pts',(-2.51363229639634,1.41266446666228E-5,
2.11258330249198));
#31532=CARTESIAN_POINT('Ctrl Pts',(-2.51365314043488,0.413200028375445,
2.08655639524664));
#31533=CARTESIAN_POINT('Ctrl Pts',(-2.41712296010665,0.826376698454607,
2.0605294880013));
#31534=CARTESIAN_POINT('Ctrl Pts',(-2.22398683849327,1.18795070900901,2.03450258075596));
#31535=CARTESIAN_POINT('Ctrl Pts',(-1.83687666966046,1.91266742746658,1.98233584791606));
#31536=CARTESIAN_POINT('Ctrl Pts',(-1.06166440870055,2.43007701911127,1.93016911507617));
#31537=CARTESIAN_POINT('Ctrl Pts',(-0.243891408049745,2.50955308940395,
1.87800238223627));
#31538=CARTESIAN_POINT('Ctrl Pts',(0.573881592601061,2.58902915969663,1.82583564939637));
#31539=CARTESIAN_POINT('Ctrl Pts',(1.43421533294277,2.23057170863728,1.77366891655648));
#31540=CARTESIAN_POINT('Ctrl Pts',(1.95362700805596,1.59395389183621,1.72150218371658));
#31541=CARTESIAN_POINT('Ctrl Pts',(2.47303868316916,0.957336075035145,1.66933545087668));
#31542=CARTESIAN_POINT('Ctrl Pts',(2.65152829305385,0.0425578924923607,
1.61716871803679));
#31543=CARTESIAN_POINT('Ctrl Pts',(2.40953581913432,-0.742620459122797,
1.56500198519689));
#31544=CARTESIAN_POINT('Ctrl Pts',(2.16754334521479,-1.52779881073796,1.51283525235699));
#31545=CARTESIAN_POINT('Ctrl Pts',(1.50506878749103,-2.1833773314255,1.4606685195171));
#31546=CARTESIAN_POINT('Ctrl Pts',(0.717402890595091,-2.41715770945467,
1.4085017866772));
#31547=CARTESIAN_POINT('Ctrl Pts',(-0.0702630063008448,-2.65093808748384,
1.35633505383731));
#31548=CARTESIAN_POINT('Ctrl Pts',(-0.983120242368966,-2.46292032285465,
1.30416832099741));
#31549=CARTESIAN_POINT('Ctrl Pts',(-1.61427588850106,-1.93687711375941,
1.25200158815751));
#31550=CARTESIAN_POINT('Ctrl Pts',(-2.17654123387562,-1.46825123921249,
1.205528826269));
#31551=CARTESIAN_POINT('Ctrl Pts',(-2.51524406302822,-0.731363410840463,
1.15905606438049));
#31552=CARTESIAN_POINT('Ctrl Pts',(-2.52025742113573,0.00144393706437333,
1.11258330249198));
#31553=CARTESIAN_POINT('Ctrl Pts',(-2.52068696412108,-0.00113551940461809,
1.38741669750803));
#31554=CARTESIAN_POINT('Ctrl Pts',(-2.52107949725397,-0.0698493560164091,
1.3917762763544));
#31555=CARTESIAN_POINT('Ctrl Pts',(-2.51850599021738,-0.138533361798365,
1.39613585520078));
#31556=CARTESIAN_POINT('Ctrl Pts',(-2.51286990332195,-0.206965106428379,
1.40049543404715));
#31557=CARTESIAN_POINT('Ctrl Pts',(-2.4454284715468,-1.02581955675002,1.45266216688705));
#31558=CARTESIAN_POINT('Ctrl Pts',(-1.93947085705393,-1.80855393755627,
1.50482889972694));
#31559=CARTESIAN_POINT('Ctrl Pts',(-1.22052386480191,-2.20627819800367,
1.55699563256684));
#31560=CARTESIAN_POINT('Ctrl Pts',(-0.501576872549894,-2.60400245845108,
1.60916236540673));
#31561=CARTESIAN_POINT('Ctrl Pts',(0.430359497461277,-2.61671659853964,
1.66132909824663));
#31562=CARTESIAN_POINT('Ctrl Pts',(1.15988750019281,-2.2387513379105,1.71349583108653));
#31563=CARTESIAN_POINT('Ctrl Pts',(1.88941550292434,-1.86078607728136,1.76566256392642));
#31564=CARTESIAN_POINT('Ctrl Pts',(2.41653513837623,-1.09214141593451,1.81782929676632));
#31565=CARTESIAN_POINT('Ctrl Pts',(2.50628871104416,-0.27543223888268,1.86999602960622));
#31566=CARTESIAN_POINT('Ctrl Pts',(2.59604228371209,0.541276938169144,1.92216276244611));
#31567=CARTESIAN_POINT('Ctrl Pts',(2.24842979359607,1.40605063092595,1.97432949528601));
#31568=CARTESIAN_POINT('Ctrl Pts',(1.61839553463159,1.93342727280644,2.02649622812591));
#31569=CARTESIAN_POINT('Ctrl Pts',(0.9883612756671,2.46080391468694,2.0786629609658));
#31570=CARTESIAN_POINT('Ctrl Pts',(0.0759052478541385,2.6507835056911,2.1308296938057));
#31571=CARTESIAN_POINT('Ctrl Pts',(-0.712256806761665,2.41868475685738,
2.1829964266456));
#31572=CARTESIAN_POINT('Ctrl Pts',(-1.50041886137746,2.18658600802365,2.23516315948549));
#31573=CARTESIAN_POINT('Ctrl Pts',(-2.16428694279611,1.53240891935204,2.28732989232539));
#31574=CARTESIAN_POINT('Ctrl Pts',(-2.40795002197348,0.747744850575128,
2.33949662516528));
#31575=CARTESIAN_POINT('Ctrl Pts',(-2.48255920772454,0.507482158922327,
2.35546998261286));
#31576=CARTESIAN_POINT('Ctrl Pts',(-2.51777110227279,0.254985358855856,
2.37144334006044));
#31577=CARTESIAN_POINT('Ctrl Pts',(-2.51584480336699,0.00196506899055149,
2.38741669750802));
#31578=CARTESIAN_POINT('Origin',(0.,0.,2.5));
#31579=CARTESIAN_POINT('',(-2.51589013302272,-0.00197902614912163,3.38741669750803));
#31580=CARTESIAN_POINT('',(-2.52021651143941,-0.00144364612508765,3.11258330249198));
#31581=CARTESIAN_POINT('',(-2.5175,3.08304831685346E-16,2.5));
#31582=CARTESIAN_POINT('Ctrl Pts',(-2.52021651143941,-0.00144364612508765,
3.11258330249198));
#31583=CARTESIAN_POINT('Ctrl Pts',(-2.51515411267109,0.729619079365268,
3.06622345895268));
#31584=CARTESIAN_POINT('Ctrl Pts',(-2.17829775808437,1.46475479323487,3.01986361541339));
#31585=CARTESIAN_POINT('Ctrl Pts',(-1.61839525002992,1.93342693235859,2.97350377187409));
#31586=CARTESIAN_POINT('Ctrl Pts',(-0.988361101417928,2.4608034807813,2.9213370390342));
#31587=CARTESIAN_POINT('Ctrl Pts',(-0.0759052345218647,2.65078303997177,
2.8691703061943));
#31588=CARTESIAN_POINT('Ctrl Pts',(0.712256681486064,2.41868433245784,2.81700357335441));
#31589=CARTESIAN_POINT('Ctrl Pts',(1.50041859749399,2.18658562494391,2.76483684051451));
#31590=CARTESIAN_POINT('Ctrl Pts',(2.16428656261379,1.53240865072558,2.71267010767461));
#31591=CARTESIAN_POINT('Ctrl Pts',(2.40794959914724,0.747744719274148,2.66050337483472));
#31592=CARTESIAN_POINT('Ctrl Pts',(2.65161263568068,-0.0369192121772903,
2.60833664199482));
#31593=CARTESIAN_POINT('Ctrl Pts',(2.47507074362777,-0.952070100861841,
2.55616990915492));
#31594=CARTESIAN_POINT('Ctrl Pts',(1.95701531533631,-1.58979072079872,2.50400317631503));
#31595=CARTESIAN_POINT('Ctrl Pts',(1.43895988704484,-2.22751134073559,2.45183644347513));
#31596=CARTESIAN_POINT('Ctrl Pts',(0.579390922514817,-2.5878016919248,2.39966971063523));
#31597=CARTESIAN_POINT('Ctrl Pts',(-0.238549412870579,-2.5100671436653,
2.34750297779534));
#31598=CARTESIAN_POINT('Ctrl Pts',(-1.05648974825598,-2.4323325954058,2.29533624495544));
#31599=CARTESIAN_POINT('Ctrl Pts',(-1.83280145449676,-1.91657314769758,
2.24316951211554));
#31600=CARTESIAN_POINT('Ctrl Pts',(-2.22145326926428,-1.19268150120826,
2.19100277927565));
#31601=CARTESIAN_POINT('Ctrl Pts',(-2.41619980794843,-0.829952222250707,
2.16486295368109));
#31602=CARTESIAN_POINT('Ctrl Pts',(-2.51361136192544,-0.414964391838591,
2.13872312808653));
#31603=CARTESIAN_POINT('Ctrl Pts',(-2.51363229639634,1.41266446666228E-5,
2.11258330249198));
#31604=CARTESIAN_POINT('Ctrl Pts',(-2.51584480336699,0.00196506899055149,
2.38741669750802));
#31605=CARTESIAN_POINT('Ctrl Pts',(-2.51148008169565,-0.571343226589796,
2.42361007290034));
#31606=CARTESIAN_POINT('Ctrl Pts',(-2.31644353295754,-1.14733917999922,
2.45980344829266));
#31607=CARTESIAN_POINT('Ctrl Pts',(-1.95701565897371,-1.58979099958587,
2.49599682368498));
#31608=CARTESIAN_POINT('Ctrl Pts',(-1.43896013986049,-2.22751173208773,
2.54816355652487));
#31609=CARTESIAN_POINT('Ctrl Pts',(-0.579391024697962,-2.58780214820923,
2.60033028936477));
#31610=CARTESIAN_POINT('Ctrl Pts',(0.238549454567511,-2.51006758543924,
2.65249702220466));
#31611=CARTESIAN_POINT('Ctrl Pts',(1.05648993383299,-2.43233302266925,2.70466375504456));
#31612=CARTESIAN_POINT('Ctrl Pts',(1.83280177720141,-1.91657348100776,2.75683048788446));
#31613=CARTESIAN_POINT('Ctrl Pts',(2.22145365982248,-1.19268170883292,2.80899722072435));
#31614=CARTESIAN_POINT('Ctrl Pts',(2.61010554244356,-0.468789936658086,
2.86116395356425));
#31615=CARTESIAN_POINT('Ctrl Pts',(2.61109746431729,0.463234066030113,2.91333068640414));
#31616=CARTESIAN_POINT('Ctrl Pts',(2.22398722823793,1.18795091427809,2.96549741924404));
#31617=CARTESIAN_POINT('Ctrl Pts',(1.83687699215856,1.91266776252607,3.01766415208394));
#31618=CARTESIAN_POINT('Ctrl Pts',(1.06166459812611,2.43007745633383,3.06983088492383));
#31619=CARTESIAN_POINT('Ctrl Pts',(0.243891452474371,2.50955353617875,3.12199761776373));
#31620=CARTESIAN_POINT('Ctrl Pts',(-0.573881693177372,2.58902961602367,
3.17416435060363));
#31621=CARTESIAN_POINT('Ctrl Pts',(-1.4342155904484,2.23057208190574,3.22633108344352));
#31622=CARTESIAN_POINT('Ctrl Pts',(-1.95362735417331,1.59395416098643,3.27849781628342));
#31623=CARTESIAN_POINT('Ctrl Pts',(-2.31512049434143,1.1508894724433,3.31480411002495));
#31624=CARTESIAN_POINT('Ctrl Pts',(-2.5114814387863,0.573092447932525,3.35111040376649));
#31625=CARTESIAN_POINT('Ctrl Pts',(-2.51589013302272,-0.00197902614912163,
3.38741669750803));
#31626=CARTESIAN_POINT('Origin',(0.,0.,2.5));
#31627=CARTESIAN_POINT('',(-2.52065797473119,0.00106685237120291,4.38741669750802));
#31628=CARTESIAN_POINT('',(-2.51644348201823,0.00207613456667446,4.11258330249198));
#31629=CARTESIAN_POINT('',(-2.5175,3.08304831685346E-16,2.5));
#31630=CARTESIAN_POINT('',(1.91346599666507,1.63598720337493,5.));
#31631=CARTESIAN_POINT('Ctrl Pts',(-2.52065797473119,0.00106685237120291,
4.38741669750802));
#31632=CARTESIAN_POINT('Ctrl Pts',(-2.51627582008385,-0.750533596725348,
4.43511093315233));
#31633=CARTESIAN_POINT('Ctrl Pts',(-2.1571958584412,-1.50553160271072,4.48280516879663));
#31634=CARTESIAN_POINT('Ctrl Pts',(-1.56924561797524,-1.97326800927033,
4.53049940444093));
#31635=CARTESIAN_POINT('Ctrl Pts',(-0.926160710476491,-2.48486610557827,
4.58266613728083));
#31636=CARTESIAN_POINT('Ctrl Pts',(-0.00926858752154605,-2.65280097461769,
4.63483287012073));
#31637=CARTESIAN_POINT('Ctrl Pts',(0.772845077643461,-2.40046275794039,
4.68699960296062));
#31638=CARTESIAN_POINT('Ctrl Pts',(1.55495874280847,-2.14812454126309,4.73916633580052));
#31639=CARTESIAN_POINT('Ctrl Pts',(2.20229395018354,-1.47551323886906,4.79133306864041));
#31640=CARTESIAN_POINT('Ctrl Pts',(2.42597897401485,-0.686281044499074,
4.84349980148031));
#31641=CARTESIAN_POINT('Ctrl Pts',(2.64966399784617,0.102951149870913,4.89566653432021));
#31642=CARTESIAN_POINT('Ctrl Pts',(2.44969883813372,1.00880423621685,4.9478332671601));
#31643=CARTESIAN_POINT('Ctrl Pts',(1.91346599666506,1.63598720337495,5.));
#31644=CARTESIAN_POINT('',(-1.91693299680257,1.63821185741719,5.));
#31645=CARTESIAN_POINT('Origin',(0.,0.,5.));
#31646=CARTESIAN_POINT('Ctrl Pts',(-1.91694926235926,1.6382222944622,5.));
#31647=CARTESIAN_POINT('Ctrl Pts',(-1.40805335272935,2.22926302987767,4.95050205137012));
#31648=CARTESIAN_POINT('Ctrl Pts',(-0.602342425840394,2.56946465859549,
4.90100410274024));
#31649=CARTESIAN_POINT('Ctrl Pts',(0.175477439781852,2.51505854463557,4.85150615411036));
#31650=CARTESIAN_POINT('Ctrl Pts',(0.995235071171573,2.45771901258696,4.79933942127047));
#31651=CARTESIAN_POINT('Ctrl Pts',(1.78401295214682,1.96207240922004,4.74717268843057));
#31652=CARTESIAN_POINT('Ctrl Pts',(2.19068546260575,1.2482867574395,4.69500595559068));
#31653=CARTESIAN_POINT('Ctrl Pts',(2.59735797306467,0.534501105658956,4.64283922275078));
#31654=CARTESIAN_POINT('Ctrl Pts',(2.62192511300726,-0.397423594535204,
4.59067248991088));
#31655=CARTESIAN_POINT('Ctrl Pts',(2.25319644256834,-1.13170027426973,4.53850575707098));
#31656=CARTESIAN_POINT('Ctrl Pts',(1.88446777212942,-1.86597695400425,4.48633902423109));
#31657=CARTESIAN_POINT('Ctrl Pts',(1.12244329130898,-2.40260561327913,4.43417229139119));
#31658=CARTESIAN_POINT('Ctrl Pts',(0.306910879222839,-2.50259532036743,
4.3820055585513));
#31659=CARTESIAN_POINT('Ctrl Pts',(-0.508621532863308,-2.60258502745572,
4.3298388257114));
#31660=CARTESIAN_POINT('Ctrl Pts',(-1.37766187621516,-2.26593578235743,
4.2776720928715));
#31661=CARTESIAN_POINT('Ctrl Pts',(-1.91291133870635,-1.64259818874412,
4.22550536003161));
#31662=CARTESIAN_POINT('Ctrl Pts',(-2.29911832868587,-1.19283157963813,
4.18786467418506));
#31663=CARTESIAN_POINT('Ctrl Pts',(-2.51154433642508,-0.59380690010991,
4.15022398833852));
#31664=CARTESIAN_POINT('Ctrl Pts',(-2.51644348201823,0.00207613456667446,
4.11258330249198));
#31665=CARTESIAN_POINT('Origin',(0.,0.,7.20842344717746));
#31666=CARTESIAN_POINT('',(-3.07686640868348,0.00176283637231212,0.791576552822548));
#31667=CARTESIAN_POINT('',(-3.06877657964135,-0.000320642608852016,0.708423447177458));
#31668=CARTESIAN_POINT('',(-3.0735,2.32747228194194E-14,7.20842344717746));
#31669=CARTESIAN_POINT('',(0.793799282532827,-2.96922295374571,0.));
#31670=CARTESIAN_POINT('Ctrl Pts',(-3.06877657964135,-0.000320642608851972,
0.708423447177458));
#31671=CARTESIAN_POINT('Ctrl Pts',(-3.06807698094575,0.532211151373012,
0.680949229477891));
#31672=CARTESIAN_POINT('Ctrl Pts',(-2.68518598576605,2.07671369914706,0.601308278938428));
#31673=CARTESIAN_POINT('Ctrl Pts',(-0.25205435815242,3.60563262622145,0.469500595559067));
#31674=CARTESIAN_POINT('Ctrl Pts',(2.8638258713055,2.21030524695087,0.313000397039378));
#31675=CARTESIAN_POINT('Ctrl Pts',(3.4222759216869,-1.16283315864926,0.15650019851969));
#31676=CARTESIAN_POINT('Ctrl Pts',(1.76703113798771,-2.70903678361537,0.0521667328398966));
#31677=CARTESIAN_POINT('Ctrl Pts',(0.793799282532827,-2.96922295374571,
0.));
#31678=CARTESIAN_POINT('',(-0.795749017144049,-2.97385877393435,2.61949253457777E-15));
#31679=CARTESIAN_POINT('Origin',(0.,0.,0.));
#31680=CARTESIAN_POINT('Ctrl Pts',(-3.07686640868348,0.00176283637231189,
0.791576552822548));
#31681=CARTESIAN_POINT('Ctrl Pts',(-3.07761631882972,0.111377919445277,
0.785882581871163));
#31682=CARTESIAN_POINT('Ctrl Pts',(-3.02309142539902,1.22449894749353,0.728021878079882));
#31683=CARTESIAN_POINT('Ctrl Pts',(-1.66998478533906,3.20643252148329,0.617994441448703));
#31684=CARTESIAN_POINT('Ctrl Pts',(1.74335679702331,3.1676297706248,0.461494242929015));
#31685=CARTESIAN_POINT('Ctrl Pts',(3.60260150316633,0.3038109312067,0.304994044409326));
#31686=CARTESIAN_POINT('Ctrl Pts',(2.27315994968988,-2.77521413120327,0.151162630099654));
#31687=CARTESIAN_POINT('Ctrl Pts',(0.124975895037349,-3.21660834551288,
0.0494979486298794));
#31688=CARTESIAN_POINT('Ctrl Pts',(-0.795758164394602,-2.97388052305263,
9.44882193321117E-16));
#31689=CARTESIAN_POINT('Origin',(0.,0.,7.20842344717746));
#31690=CARTESIAN_POINT('',(-3.06877809850016,1.72465709349923E-5,1.79157655282255));
#31691=CARTESIAN_POINT('',(-3.0773908179647,-0.00138630343203515,1.70842344717746));
#31692=CARTESIAN_POINT('',(-3.0735,2.32747228194194E-14,7.20842344717746));
#31693=CARTESIAN_POINT('Ctrl Pts',(-3.0773908179647,-0.00138630343203517,
1.70842344717746));
#31694=CARTESIAN_POINT('Ctrl Pts',(-3.07213562808389,0.918546890942566,
1.66061629318394));
#31695=CARTESIAN_POINT('Ctrl Pts',(-2.15053865242723,2.85146124051564,1.56064240635052));
#31696=CARTESIAN_POINT('Ctrl Pts',(1.11551761111489,3.4389870765969,1.4085017866772));
#31697=CARTESIAN_POINT('Ctrl Pts',(3.48075054753741,0.977649178608381,1.25200158815752));
#31698=CARTESIAN_POINT('Ctrl Pts',(2.74289601575609,-2.35537719050612,1.09550138963782));
#31699=CARTESIAN_POINT('Ctrl Pts',(-0.440018957118456,-3.58837739167123,
0.939001191118136));
#31700=CARTESIAN_POINT('Ctrl Pts',(-2.74101688880118,-1.96797948390379,
0.809975210298013));
#31701=CARTESIAN_POINT('Ctrl Pts',(-3.06940534554735,-0.47893479386132,
0.733115962317788));
#31702=CARTESIAN_POINT('Ctrl Pts',(-3.06877657964135,-0.000320642608851972,
0.708423447177458));
#31703=CARTESIAN_POINT('Ctrl Pts',(-3.06877809850016,1.72465709353392E-5,
1.79157655282255));
#31704=CARTESIAN_POINT('Ctrl Pts',(-3.06880354602845,0.504456916469473,
1.76554964557721));
#31705=CARTESIAN_POINT('Ctrl Pts',(-2.71474447759704,2.01993058914264,1.68735600549197));
#31706=CARTESIAN_POINT('Ctrl Pts',(-0.349716256635896,3.59845088308181,
1.55699563256684));
#31707=CARTESIAN_POINT('Ctrl Pts',(2.8013094644448,2.28557822072128,1.40049543404715));
#31708=CARTESIAN_POINT('Ctrl Pts',(3.45503873870173,-1.0648536490447,1.24399523552746));
#31709=CARTESIAN_POINT('Ctrl Pts',(1.02868455419652,-3.46595066989846,1.08749503700777));
#31710=CARTESIAN_POINT('Ctrl Pts',(-2.1930684252685,-2.80237835053392,0.936688809439468));
#31711=CARTESIAN_POINT('Ctrl Pts',(-3.07074583027496,-0.892887961556386,
0.83804931471106));
#31712=CARTESIAN_POINT('Ctrl Pts',(-3.07686640868348,0.00176283637231189,
0.791576552822548));
#31713=CARTESIAN_POINT('Origin',(0.,0.,7.20842344717746));
#31714=CARTESIAN_POINT('',(-3.0768164639162,-0.00176248117795978,2.79157655282255));
#31715=CARTESIAN_POINT('',(-3.07147924653364,0.00239906238030041,2.70842344717746));
#31716=CARTESIAN_POINT('',(-3.0735,2.32747228194194E-14,7.20842344717746));
#31717=CARTESIAN_POINT('Ctrl Pts',(-3.07147924653364,0.00239906238030076,
2.70842344717746));
#31718=CARTESIAN_POINT('Ctrl Pts',(-3.07383097630006,0.311299900871277,
2.69245008972988));
#31719=CARTESIAN_POINT('Ctrl Pts',(-2.89044774320411,1.62630098606235,2.6243099994424));
#31720=CARTESIAN_POINT('Ctrl Pts',(-1.02130638419203,3.46815705171515,2.50400317631503));
#31721=CARTESIAN_POINT('Ctrl Pts',(2.32062044975012,2.77234500847627,2.34750297779534));
#31722=CARTESIAN_POINT('Ctrl Pts',(3.59377276955738,-0.394942313892847,
2.19100277927565));
#31723=CARTESIAN_POINT('Ctrl Pts',(1.66316438874938,-3.21015109242256,2.03450258075596));
#31724=CARTESIAN_POINT('Ctrl Pts',(-1.7501104075517,-3.16358476523821,1.87800238223627));
#31725=CARTESIAN_POINT('Ctrl Pts',(-3.03713246509983,-1.17251597915295,
1.7693093377101));
#31726=CARTESIAN_POINT('Ctrl Pts',(-3.0778700436187,-0.0852758672160755,
1.71278302602383));
#31727=CARTESIAN_POINT('Ctrl Pts',(-3.0773908179647,-0.00138630343203517,
1.70842344717746));
#31728=CARTESIAN_POINT('Ctrl Pts',(-3.0768164639162,-0.00176248117795985,
2.79157655282255));
#31729=CARTESIAN_POINT('Ctrl Pts',(-3.0706360140197,0.890758387459429,2.74521670928325));
#31730=CARTESIAN_POINT('Ctrl Pts',(-2.19661894703825,2.79816239430364,2.64669013290406));
#31731=CARTESIAN_POINT('Ctrl Pts',(1.02130620401276,3.46815644429995,2.49599682368497));
#31732=CARTESIAN_POINT('Ctrl Pts',(3.45276382958855,1.07219267437738,2.33949662516528));
#31733=CARTESIAN_POINT('Ctrl Pts',(2.8061681927767,-2.27960425476498,2.18299642664559));
#31734=CARTESIAN_POINT('Ctrl Pts',(-0.34205648942751,-3.59919002761108,
2.02649622812591));
#31735=CARTESIAN_POINT('Ctrl Pts',(-2.71249040954675,-2.02434105954679,
1.89602293685156));
#31736=CARTESIAN_POINT('Ctrl Pts',(-3.06875254056717,-0.506610946699481,
1.8177163784171));
#31737=CARTESIAN_POINT('Ctrl Pts',(-3.06877809850016,1.72465709353392E-5,
1.79157655282255));
#31738=CARTESIAN_POINT('Origin',(0.,0.,7.20842344717746));
#31739=CARTESIAN_POINT('',(-3.0722101457728,0.00253465723558749,3.79157655282255));
#31740=CARTESIAN_POINT('',(-3.07153458742615,-0.00241610203352894,3.70842344717746));
#31741=CARTESIAN_POINT('',(-3.0735,2.32747228194194E-14,7.20842344717746));
#31742=CARTESIAN_POINT('Ctrl Pts',(-3.07153458742615,-0.00241610203352869,
3.70842344717746));
#31743=CARTESIAN_POINT('Ctrl Pts',(-3.06615221533653,0.699662219948585,
3.67211715343592));
#31744=CARTESIAN_POINT('Ctrl Pts',(-2.48197069074528,2.41863106906089,3.58364412685449));
#31745=CARTESIAN_POINT('Ctrl Pts',(0.349716325434694,3.59845154159293,3.44300436743317));
#31746=CARTESIAN_POINT('Ctrl Pts',(3.18897983255535,1.70340642470933,3.28650416891347));
#31747=CARTESIAN_POINT('Ctrl Pts',(3.18534685712864,-1.71018933171035,3.13000397039378));
#31748=CARTESIAN_POINT('Ctrl Pts',(0.342056548577105,-3.59919066394061,
2.9735037718741));
#31749=CARTESIAN_POINT('Ctrl Pts',(-2.48484176394183,-2.41428958805909,
2.83297693080198));
#31750=CARTESIAN_POINT('Ctrl Pts',(-3.06615055852694,-0.697526676037249,
2.74461682256977));
#31751=CARTESIAN_POINT('Ctrl Pts',(-3.07147924653364,0.00239906238030076,
2.70842344717746));
#31752=CARTESIAN_POINT('Ctrl Pts',(-3.0722101457728,0.00253465723558725,
3.79157655282255));
#31753=CARTESIAN_POINT('Ctrl Pts',(-3.0745183487722,0.283281367407046,3.77705050582919));
#31754=CARTESIAN_POINT('Ctrl Pts',(-2.91187546114467,1.56963838731655,3.71035772599594));
#31755=CARTESIAN_POINT('Ctrl Pts',(-1.11551737463701,3.43898632522653,3.5914982133228));
#31756=CARTESIAN_POINT('Ctrl Pts',(2.24412684766706,2.83462531411003,3.43499801480311));
#31757=CARTESIAN_POINT('Ctrl Pts',(3.60321095550619,-0.296771509319279,
3.27849781628342));
#31758=CARTESIAN_POINT('Ctrl Pts',(1.75011009124083,-3.16358418358746,3.12199761776373));
#31759=CARTESIAN_POINT('Ctrl Pts',(-1.66316409145381,-3.2101505430571,2.96549741924404));
#31760=CARTESIAN_POINT('Ctrl Pts',(-3.02187071265548,-1.22888761088956,
2.85535706426364));
#31761=CARTESIAN_POINT('Ctrl Pts',(-3.07759060777944,-0.113556859393683,
2.79738344212315));
#31762=CARTESIAN_POINT('Ctrl Pts',(-3.0768164639162,-0.00176248117795985,
2.79157655282255));
#31763=CARTESIAN_POINT('Origin',(0.,0.,7.20842344717746));
#31764=CARTESIAN_POINT('',(-3.07018609065268,-0.00333738419709156,4.79157655282255));
#31765=CARTESIAN_POINT('',(-3.07735542615147,0.00130247100806778,4.70842344717746));
#31766=CARTESIAN_POINT('',(-3.0735,2.32747228194194E-14,7.20842344717746));
#31767=CARTESIAN_POINT('',(-0.793799282532885,-2.96922295374569,5.));
#31768=CARTESIAN_POINT('Ctrl Pts',(-0.793799282532885,-2.96922295374569,
5.));
#31769=CARTESIAN_POINT('Ctrl Pts',(-1.76703113798775,-2.70903678361534,
4.9478332671601));
#31770=CARTESIAN_POINT('Ctrl Pts',(-2.8692411723445,-1.67944397566504,4.87835878476762));
#31771=CARTESIAN_POINT('Ctrl Pts',(-3.07242022864685,-0.338323361726583,
4.80888430237514));
#31772=CARTESIAN_POINT('Ctrl Pts',(-3.07018609065268,-0.00333738419709143,
4.79157655282255));
#31773=CARTESIAN_POINT('',(0.795750420935782,-2.97385779503552,5.));
#31774=CARTESIAN_POINT('Origin',(0.,0.,5.));
#31775=CARTESIAN_POINT('Ctrl Pts',(0.795759619474687,-2.97387964574988,
5.));
#31776=CARTESIAN_POINT('Ctrl Pts',(-0.124974018843371,-3.21660711871812,
4.95050205137012));
#31777=CARTESIAN_POINT('Ctrl Pts',(-2.17865809628841,-2.79463535584754,
4.85330986709594));
#31778=CARTESIAN_POINT('Ctrl Pts',(-3.0720054550259,-0.916291960093509,
4.75611768282176));
#31779=CARTESIAN_POINT('Ctrl Pts',(-3.07735542615147,0.00130247100806802,
4.70842344717746));
#31780=CARTESIAN_POINT('Origin',(0.,0.,7.20842344717746));
#31781=CARTESIAN_POINT('Ctrl Pts',(-3.07735542615147,0.00130247100806811,
4.70842344717746));
#31782=CARTESIAN_POINT('Ctrl Pts',(-3.07785711635642,0.0873493163837036,
4.70395094998186));
#31783=CARTESIAN_POINT('Ctrl Pts',(-3.03598706278426,1.17657551893794,4.64731171994637));
#31784=CARTESIAN_POINT('Ctrl Pts',(-1.74335774093941,3.16762915537798,4.53850575707099));
#31785=CARTESIAN_POINT('Ctrl Pts',(1.66998541626837,3.20643379740356,4.3820055585513));
#31786=CARTESIAN_POINT('Ctrl Pts',(3.59460935228705,0.387380778120988,4.22550536003161));
#31787=CARTESIAN_POINT('Ctrl Pts',(2.31471223100892,-2.77732417593505,4.06900516151192));
#31788=CARTESIAN_POINT('Ctrl Pts',(-1.02868478492208,-3.46595142305511,
3.91250496299223));
#31789=CARTESIAN_POINT('Ctrl Pts',(-2.89215223470734,-1.62188152779685,
3.79231105821408));
#31790=CARTESIAN_POINT('Ctrl Pts',(-3.07388588181438,-0.309119687570202,
3.72428388627582));
#31791=CARTESIAN_POINT('Ctrl Pts',(-3.07153458742615,-0.00241610203352869,
3.70842344717746));
#31792=CARTESIAN_POINT('Ctrl Pts',(-3.07018609065268,-0.00333738419709143,
4.79157655282255));
#31793=CARTESIAN_POINT('Ctrl Pts',(-3.06568638497092,0.671347129621605,
4.75671756953524));
#31794=CARTESIAN_POINT('Ctrl Pts',(-2.51923155566346,2.36462266851063,4.66969185340803));
#31795=CARTESIAN_POINT('Ctrl Pts',(0.252054090990421,3.60562829022214,4.53049940444094));
#31796=CARTESIAN_POINT('Ctrl Pts',(3.14100203598835,1.79029184281612,4.37399920592124));
#31797=CARTESIAN_POINT('Ctrl Pts',(3.23098071080095,-1.62294021205589,4.21749900740156));
#31798=CARTESIAN_POINT('Ctrl Pts',(0.440018754334274,-3.58837598279832,
4.06099880888186));
#31799=CARTESIAN_POINT('Ctrl Pts',(-2.44746347564723,-2.46982179783519,
3.91902465735553));
#31800=CARTESIAN_POINT('Ctrl Pts',(-3.06622900417178,-0.724951542199748,
3.82921723866909));
#31801=CARTESIAN_POINT('Ctrl Pts',(-3.0722101457728,0.00253465723558725,
3.79157655282255));
#31802=CARTESIAN_POINT('Ctrl Pts',(1.91346599666506,1.63598720337495,5.));
#31803=CARTESIAN_POINT('Ctrl Pts',(2.44969883813372,1.00880423621685,4.9478332671601));
#31804=CARTESIAN_POINT('Ctrl Pts',(2.84962915755861,-0.802901936475035,
4.84349980148031));
#31805=CARTESIAN_POINT('Ctrl Pts',(0.907623535433406,-2.82073584365711,
4.68699960296062));
#31806=CARTESIAN_POINT('Ctrl Pts',(-1.84305283343144,-2.31693123653885,
4.53049940444093));
#31807=CARTESIAN_POINT('Ctrl Pts',(-2.95088590955911,0.248852734190564,
4.37399920592124));
#31808=CARTESIAN_POINT('Ctrl Pts',(-1.42798214179762,2.59460107325983,4.21749900740156));
#31809=CARTESIAN_POINT('Ctrl Pts',(1.36788296256894,2.62638590693459,4.06099880888186));
#31810=CARTESIAN_POINT('Ctrl Pts',(2.94434001769405,0.317303110108862,3.90449861036218));
#31811=CARTESIAN_POINT('Ctrl Pts',(1.89597788891003,-2.27490275351114,3.74799841184249));
#31812=CARTESIAN_POINT('Ctrl Pts',(-0.842594418754297,-2.8389564690227,
3.5914982133228));
#31813=CARTESIAN_POINT('Ctrl Pts',(-2.83001837825583,-0.872220375374214,
3.43499801480311));
#31814=CARTESIAN_POINT('Ctrl Pts',(-2.29454948771943,1.8721145477878,3.27849781628342));
#31815=CARTESIAN_POINT('Ctrl Pts',(0.286452204093653,2.9474871501416,3.12199761776373));
#31816=CARTESIAN_POINT('Ctrl Pts',(2.61208938619102,1.39525806871831,2.96549741924404));
#31817=CARTESIAN_POINT('Ctrl Pts',(2.60911362056983,-1.40081393934628,2.80899722072436));
#31818=CARTESIAN_POINT('Ctrl Pts',(0.280178090464571,-2.94809256433073,
2.65249702220466));
#31819=CARTESIAN_POINT('Ctrl Pts',(-2.29852925502302,-1.86722131596623,
2.49599682368498));
#31820=CARTESIAN_POINT('Ctrl Pts',(-2.82815502421476,0.878231830680435,
2.33949662516528));
#31821=CARTESIAN_POINT('Ctrl Pts',(-0.83655077995882,2.84076309669526,2.1829964266456));
#31822=CARTESIAN_POINT('Ctrl Pts',(1.90081730348005,2.27082432368278,2.02649622812591));
#31823=CARTESIAN_POINT('Ctrl Pts',(2.94365477382811,-0.323496754587683,
1.86999602960622));
#31824=CARTESIAN_POINT('Ctrl Pts',(1.36229586747244,-2.6294307386282,1.71349583108653));
#31825=CARTESIAN_POINT('Ctrl Pts',(-1.43351324256106,-2.59128831836252,
1.55699563256684));
#31826=CARTESIAN_POINT('Ctrl Pts',(-2.95138608603967,-0.243085175943775,
1.40049543404715));
#31827=CARTESIAN_POINT('Ctrl Pts',(-1.83816183321196,2.32183838356734,1.24399523552746));
#31828=CARTESIAN_POINT('Ctrl Pts',(0.913719077918246,2.81687000661548,1.08749503700777));
#31829=CARTESIAN_POINT('Ctrl Pts',(2.85107841334811,0.800791217552173,0.930994838488081));
#31830=CARTESIAN_POINT('Ctrl Pts',(2.24670269063477,-1.92928650629548,0.774494639968393));
#31831=CARTESIAN_POINT('Ctrl Pts',(-0.360418976588814,-2.93923542656005,
0.617994441448702));
#31832=CARTESIAN_POINT('Ctrl Pts',(-2.64649260465595,-1.32934744147468,
0.461494242929014));
#31833=CARTESIAN_POINT('Ctrl Pts',(-2.57279134224077,1.46642423733366,0.304994044409324));
#31834=CARTESIAN_POINT('Ctrl Pts',(-0.206457409028375,2.95336916756547,
0.148493845889635));
#31835=CARTESIAN_POINT('Ctrl Pts',(2.34575618383328,1.81045825905282,-0.00800635263005447));
#31836=CARTESIAN_POINT('Ctrl Pts',(2.80318192056183,-0.952475183634134,
-0.164506551149743));
#31837=CARTESIAN_POINT('Ctrl Pts',(1.44737299166554,-2.21896863600185,-0.268840016829536));
#31838=CARTESIAN_POINT('Ctrl Pts',(0.650199997975074,-2.43208680203508,
-0.321006749669432));
#31839=CARTESIAN_POINT('Ctrl Pts',(2.05433155034209,1.75642532122685,5.10700224988981));
#31840=CARTESIAN_POINT('Ctrl Pts',(2.63004078503903,1.08307039382514,5.05483551704991));
#31841=CARTESIAN_POINT('Ctrl Pts',(3.05941317763178,-0.862009977081469,
4.95050205137012));
#31842=CARTESIAN_POINT('Ctrl Pts',(0.974440971474582,-3.02839279553707,
4.79400185285044));
#31843=CARTESIAN_POINT('Ctrl Pts',(-1.97873471034476,-2.48749909718309,
4.63750165433074));
#31844=CARTESIAN_POINT('Ctrl Pts',(-3.16812424993844,0.26717277658844,4.48100145581105));
#31845=CARTESIAN_POINT('Ctrl Pts',(-1.53310734151155,2.78561043396588,4.32450125729137));
#31846=CARTESIAN_POINT('Ctrl Pts',(1.46858378046875,2.81973520375758,4.16800105877167));
#31847=CARTESIAN_POINT('Ctrl Pts',(3.16109646255838,0.34066233277957,4.01150086025199));
#31848=CARTESIAN_POINT('Ctrl Pts',(2.03555600294299,-2.44237656098578,3.8550006617323));
#31849=CARTESIAN_POINT('Ctrl Pts',(-0.904624540810224,-3.0479547870335,
3.69850046321261));
#31850=CARTESIAN_POINT('Ctrl Pts',(-3.03835869183547,-0.936431501320334,
3.54200026469292));
#31851=CARTESIAN_POINT('Ctrl Pts',(-2.46346964861608,2.00993589020025,3.38550006617323));
#31852=CARTESIAN_POINT('Ctrl Pts',(0.307540244540666,3.16447528062537,3.22899986765354));
#31853=CARTESIAN_POINT('Ctrl Pts',(2.8043862016458,1.49797418738198,3.07249966913385));
#31854=CARTESIAN_POINT('Ctrl Pts',(2.80119136608943,-1.50393907013431,2.91599947061416));
#31855=CARTESIAN_POINT('Ctrl Pts',(0.300804243168747,-3.16512526420069,
2.75949927209447));
#31856=CARTESIAN_POINT('Ctrl Pts',(-2.46774239845802,-2.0046824284028,2.60299907357478));
#31857=CARTESIAN_POINT('Ctrl Pts',(-3.03635816138303,0.942885507987068,
2.44649887505509));
#31858=CARTESIAN_POINT('Ctrl Pts',(-0.898135981369886,3.04989441503522,
2.28999867653541));
#31859=CARTESIAN_POINT('Ctrl Pts',(2.04075168557006,2.43799788528061,2.13349847801572));
#31860=CARTESIAN_POINT('Ctrl Pts',(3.16036077240454,-0.347311941022739,
1.97699827949603));
#31861=CARTESIAN_POINT('Ctrl Pts',(1.46258537456475,-2.82300418989299,1.82049808097634));
#31862=CARTESIAN_POINT('Ctrl Pts',(-1.53904563089127,-2.78205380065442,
1.66399788245665));
#31863=CARTESIAN_POINT('Ctrl Pts',(-3.16866124841479,-0.260980622196635,
1.50749768393696));
#31864=CARTESIAN_POINT('Ctrl Pts',(-1.9734836444355,2.49276749859725,1.35099748541727));
#31865=CARTESIAN_POINT('Ctrl Pts',(0.98098525565046,3.02424236327596,1.19449728689758));
#31866=CARTESIAN_POINT('Ctrl Pts',(3.06096912474454,0.859743871237576,1.03799708837789));
#31867=CARTESIAN_POINT('Ctrl Pts',(2.41210046567521,-2.0713167343657,0.881496889858203));
#31868=CARTESIAN_POINT('Ctrl Pts',(-0.386952303432029,-3.15561608159711,
0.724996691338513));
#31869=CARTESIAN_POINT('Ctrl Pts',(-2.84132211649822,-1.42721135110194,
0.568496492818825));
#31870=CARTESIAN_POINT('Ctrl Pts',(-2.76219511400983,1.57437946751671,0.411996294299135));
#31871=CARTESIAN_POINT('Ctrl Pts',(-0.221656392069724,3.1707903204508,0.255496095779446));
#31872=CARTESIAN_POINT('Ctrl Pts',(2.51844607965735,1.94374058835217,0.0989958972597565));
#31873=CARTESIAN_POINT('Ctrl Pts',(3.00954658760352,-1.02259450863918,-0.0575043012599319));
#31874=CARTESIAN_POINT('Ctrl Pts',(1.55392570710626,-2.38232468520636,-0.161837766939725));
#31875=CARTESIAN_POINT('Ctrl Pts',(0.698066426160992,-2.61113218593862,
-0.214004499779622));
#31876=CARTESIAN_POINT('Ctrl Pts',(2.19519710401912,1.87686343907875,5.21400449977962));
#31877=CARTESIAN_POINT('Ctrl Pts',(2.81038273194434,1.15733655143342,5.16183776693973));
#31878=CARTESIAN_POINT('Ctrl Pts',(3.26919719770494,-0.921118017687907,
5.05750430125993));
#31879=CARTESIAN_POINT('Ctrl Pts',(1.04125840751576,-3.23604974741702,4.90100410274025));
#31880=CARTESIAN_POINT('Ctrl Pts',(-2.11441658725808,-2.65806695782732,
4.74450390422055));
#31881=CARTESIAN_POINT('Ctrl Pts',(-3.38536259031776,0.285492818986313,
4.58800370570087));
#31882=CARTESIAN_POINT('Ctrl Pts',(-1.63823254122548,2.97661979467193,4.43150350718118));
#31883=CARTESIAN_POINT('Ctrl Pts',(1.56928459836856,3.01308450058056,4.27500330866148));
#31884=CARTESIAN_POINT('Ctrl Pts',(3.37785290742272,0.364021555450283,4.1185031101418));
#31885=CARTESIAN_POINT('Ctrl Pts',(2.17513411697596,-2.60985036846042,3.96200291162211));
#31886=CARTESIAN_POINT('Ctrl Pts',(-0.966654662866148,-3.25695310504431,
3.80550271310242));
#31887=CARTESIAN_POINT('Ctrl Pts',(-3.24669900541512,-1.00064262726645,
3.64900251458273));
#31888=CARTESIAN_POINT('Ctrl Pts',(-2.63238980951274,2.1477572326127,3.49250231606304));
#31889=CARTESIAN_POINT('Ctrl Pts',(0.328628284987678,3.38146341110915,3.33600211754336));
#31890=CARTESIAN_POINT('Ctrl Pts',(2.99668301710058,1.60069030604565,3.17950191902366));
#31891=CARTESIAN_POINT('Ctrl Pts',(2.99326911160904,-1.60706420092233,3.02300172050398));
#31892=CARTESIAN_POINT('Ctrl Pts',(0.321430395872926,-3.38215796407065,
2.86650152198428));
#31893=CARTESIAN_POINT('Ctrl Pts',(-2.63695554189302,-2.14214354083938,
2.71000132346459));
#31894=CARTESIAN_POINT('Ctrl Pts',(-3.24456129855131,1.0075391852937,2.55350112494491));
#31895=CARTESIAN_POINT('Ctrl Pts',(-0.959721182780959,3.25902573337519,
2.39700092642522));
#31896=CARTESIAN_POINT('Ctrl Pts',(2.18068606766009,2.60517144687844,2.24050072790553));
#31897=CARTESIAN_POINT('Ctrl Pts',(3.37706677098096,-0.371127127457793,
2.08400052938584));
#31898=CARTESIAN_POINT('Ctrl Pts',(1.56287488165706,-3.01657764115777,1.92750033086615));
#31899=CARTESIAN_POINT('Ctrl Pts',(-1.64457801922149,-2.97281928294631,
1.77100013234646));
#31900=CARTESIAN_POINT('Ctrl Pts',(-3.3859364107899,-0.278876068449496,
1.61449993382677));
#31901=CARTESIAN_POINT('Ctrl Pts',(-2.10880545565905,2.66369661362717,1.45799973530708));
#31902=CARTESIAN_POINT('Ctrl Pts',(1.04825143338267,3.23161471993643,1.30149953678739));
#31903=CARTESIAN_POINT('Ctrl Pts',(3.27085983614097,0.918696524922978,1.1449993382677));
#31904=CARTESIAN_POINT('Ctrl Pts',(2.57749824071565,-2.21334696243591,0.988499139748014));
#31905=CARTESIAN_POINT('Ctrl Pts',(-0.413485630275245,-3.37199673663417,
0.831998941228324));
#31906=CARTESIAN_POINT('Ctrl Pts',(-3.03615162834048,-1.52507526072921,
0.675498742708636));
#31907=CARTESIAN_POINT('Ctrl Pts',(-2.9515988857789,1.68233469769977,0.518998544188945));
#31908=CARTESIAN_POINT('Ctrl Pts',(-0.23685537511107,3.38821147333612,0.362498345669257));
#31909=CARTESIAN_POINT('Ctrl Pts',(2.69113597548142,2.07702291765152,0.205998147149567));
#31910=CARTESIAN_POINT('Ctrl Pts',(3.21591125464521,-1.09271383364422,0.049497948629879));
#31911=CARTESIAN_POINT('Ctrl Pts',(1.66047842254699,-2.54568073441086,-0.0548355170499141));
#31912=CARTESIAN_POINT('Ctrl Pts',(0.745932854346909,-2.79017756984216,
-0.107002249889811));
#31913=CARTESIAN_POINT('Ctrl Pts',(2.33606265769615,1.99730155693065,5.32100674966943));
#31914=CARTESIAN_POINT('Ctrl Pts',(2.99072467884965,1.23160270904171,5.26884001682954));
#31915=CARTESIAN_POINT('Ctrl Pts',(3.47898121777811,-0.980226058294341,
5.16450655114975));
#31916=CARTESIAN_POINT('Ctrl Pts',(1.10807584355693,-3.44370669929698,5.00800635263005));
#31917=CARTESIAN_POINT('Ctrl Pts',(-2.25009846417141,-2.82863481847156,
4.85150615411037));
#31918=CARTESIAN_POINT('Ctrl Pts',(-3.60260093069709,0.30381286138419,4.69500595559067));
#31919=CARTESIAN_POINT('Ctrl Pts',(-1.74335774093941,3.16762915537798,4.53850575707099));
#31920=CARTESIAN_POINT('Ctrl Pts',(1.66998541626837,3.20643379740356,4.3820055585513));
#31921=CARTESIAN_POINT('Ctrl Pts',(3.59460935228705,0.387380778120988,4.22550536003161));
#31922=CARTESIAN_POINT('Ctrl Pts',(2.31471223100892,-2.77732417593505,4.06900516151192));
#31923=CARTESIAN_POINT('Ctrl Pts',(-1.02868478492208,-3.46595142305511,
3.91250496299223));
#31924=CARTESIAN_POINT('Ctrl Pts',(-3.45503931899475,-1.06485375321257,
3.75600476447254));
#31925=CARTESIAN_POINT('Ctrl Pts',(-2.8013099704094,2.28557857502515,3.59950456595285));
#31926=CARTESIAN_POINT('Ctrl Pts',(0.349716325434694,3.59845154159293,3.44300436743317));
#31927=CARTESIAN_POINT('Ctrl Pts',(3.18897983255535,1.70340642470933,3.28650416891347));
#31928=CARTESIAN_POINT('Ctrl Pts',(3.18534685712864,-1.71018933171035,3.13000397039378));
#31929=CARTESIAN_POINT('Ctrl Pts',(0.342056548577105,-3.59919066394061,
2.9735037718741));
#31930=CARTESIAN_POINT('Ctrl Pts',(-2.80616868532801,-2.27960465327595,
2.8170035733544));
#31931=CARTESIAN_POINT('Ctrl Pts',(-3.45276443571958,1.07219286260033,2.66050337483472));
#31932=CARTESIAN_POINT('Ctrl Pts',(-1.02130638419203,3.46815705171515,2.50400317631503));
#31933=CARTESIAN_POINT('Ctrl Pts',(2.32062044975012,2.77234500847627,2.34750297779534));
#31934=CARTESIAN_POINT('Ctrl Pts',(3.59377276955738,-0.394942313892847,
2.19100277927565));
#31935=CARTESIAN_POINT('Ctrl Pts',(1.66316438874938,-3.21015109242256,2.03450258075596));
#31936=CARTESIAN_POINT('Ctrl Pts',(-1.7501104075517,-3.16358476523821,1.87800238223627));
#31937=CARTESIAN_POINT('Ctrl Pts',(-3.60321157316502,-0.296771514702359,
1.72150218371658));
#31938=CARTESIAN_POINT('Ctrl Pts',(-2.2441272668826,2.83462572865708,1.56500198519689));
#31939=CARTESIAN_POINT('Ctrl Pts',(1.11551761111489,3.4389870765969,1.4085017866772));
#31940=CARTESIAN_POINT('Ctrl Pts',(3.48075054753741,0.977649178608381,1.25200158815752));
#31941=CARTESIAN_POINT('Ctrl Pts',(2.74289601575609,-2.35537719050612,1.09550138963782));
#31942=CARTESIAN_POINT('Ctrl Pts',(-0.440018957118456,-3.58837739167123,
0.939001191118136));
#31943=CARTESIAN_POINT('Ctrl Pts',(-3.23098114018275,-1.62293917035647,
0.782500992598446));
#31944=CARTESIAN_POINT('Ctrl Pts',(-3.14100265754796,1.79028992788282,0.626000794078757));
#31945=CARTESIAN_POINT('Ctrl Pts',(-0.25205435815242,3.60563262622145,0.469500595559067));
#31946=CARTESIAN_POINT('Ctrl Pts',(2.8638258713055,2.21030524695087,0.313000397039378));
#31947=CARTESIAN_POINT('Ctrl Pts',(3.4222759216869,-1.16283315864926,0.15650019851969));
#31948=CARTESIAN_POINT('Ctrl Pts',(1.76703113798771,-2.70903678361537,0.0521667328398966));
#31949=CARTESIAN_POINT('Ctrl Pts',(0.793799282532827,-2.96922295374571,
0.));
#31950=CARTESIAN_POINT('Ctrl Pts',(0.793799282532827,-2.96922295374571,
0.));
#31951=CARTESIAN_POINT('Ctrl Pts',(0.886893769048896,-2.93516857472777,
6.49317190359092E-17));
#31952=CARTESIAN_POINT('Ctrl Pts',(0.977926242508662,-2.8963539026744,3.5899553935387E-16));
#31953=CARTESIAN_POINT('Ctrl Pts',(1.06668623690149,-2.85310458823344,2.77555756156289E-16));
#31954=CARTESIAN_POINT('Ctrl Pts',(1.1573833631875,-2.8089113842966,1.94338600140189E-16));
#31955=CARTESIAN_POINT('Ctrl Pts',(1.24570840723307,-2.76008724482105,8.94098625496742E-16));
#31956=CARTESIAN_POINT('Ctrl Pts',(1.33140791312673,-2.70693413976456,1.38777878078145E-15));
#31957=CARTESIAN_POINT('Ctrl Pts',(1.41293443628286,-2.65636922920854,1.85742007207992E-15));
#31958=CARTESIAN_POINT('Ctrl Pts',(1.49208510125195,-2.60188577643099,1.19996770961849E-15));
#31959=CARTESIAN_POINT('Ctrl Pts',(1.5686100025003,-2.54371483646266,1.16573417585641E-15));
#31960=CARTESIAN_POINT('Ctrl Pts',(1.63556929109261,-2.49281526399038,1.1357798338146E-15));
#31961=CARTESIAN_POINT('Ctrl Pts',(1.70051795047849,-2.43909179704035,4.6524848618713E-16));
#31962=CARTESIAN_POINT('Ctrl Pts',(1.7632650317936,-2.38268698713509,5.55111512312578E-16));
#31963=CARTESIAN_POINT('Ctrl Pts',(1.77895111395862,-2.36858640326518,5.7757628329248E-16));
#31964=CARTESIAN_POINT('Ctrl Pts',(1.79450367669767,-2.35431414158982,1.61759689860544E-15));
#31965=CARTESIAN_POINT('Ctrl Pts',(1.80989558143071,-2.33989519409729,1.66533453693773E-15));
#31966=CARTESIAN_POINT('Ctrl Pts',(1.88231905248557,-2.27204977506178,1.88995426581157E-15));
#31967=CARTESIAN_POINT('Ctrl Pts',(1.95127638915324,-2.2008843069976,9.33280417709878E-16));
#31968=CARTESIAN_POINT('Ctrl Pts',(2.01652605934852,-2.12668615788006,7.49400541621981E-16));
#31969=CARTESIAN_POINT('Ctrl Pts',(2.08140793958276,-2.05290623822316,5.66557133186095E-16));
#31970=CARTESIAN_POINT('Ctrl Pts',(2.14262432088329,-1.97612693884884,9.5775323130718E-16));
#31971=CARTESIAN_POINT('Ctrl Pts',(2.19989413197892,-1.89660402190249,6.93889390390723E-16));
#31972=CARTESIAN_POINT('Ctrl Pts',(2.25380415733742,-1.82174638945804,4.45505362525734E-16));
#31973=CARTESIAN_POINT('Ctrl Pts',(2.30421707668655,-1.74445688295852,3.26466360005673E-15));
#31974=CARTESIAN_POINT('Ctrl Pts',(2.35085702030783,-1.6649361419825,3.7470027081099E-15));
#31975=CARTESIAN_POINT('Ctrl Pts',(2.38695907926369,-1.60338241236736,4.12036154098178E-15));
#31976=CARTESIAN_POINT('Ctrl Pts',(2.42079974187715,-1.54049148436203,2.76023327184715E-15));
#31977=CARTESIAN_POINT('Ctrl Pts',(2.45223230030139,-1.47635450699168,2.80331313717852E-15));
#31978=CARTESIAN_POINT('Ctrl Pts',(2.45885027647649,-1.46285077043765,2.81238339861069E-15));
#31979=CARTESIAN_POINT('Ctrl Pts',(2.46536173765269,-1.4492909927482,2.25462528933555E-15));
#31980=CARTESIAN_POINT('Ctrl Pts',(2.47175843746063,-1.43569095783397,2.27595720048157E-15));
#31981=CARTESIAN_POINT('Ctrl Pts',(2.51224387039329,-1.34961480639136,2.41096926669652E-15));
#31982=CARTESIAN_POINT('Ctrl Pts',(2.5482055573203,-1.26178852463594,3.62029001511052E-15));
#31983=CARTESIAN_POINT('Ctrl Pts',(2.57938539343216,-1.17245068676435,3.44169137633799E-15));
#31984=CARTESIAN_POINT('Ctrl Pts',(2.61056522954403,-1.08311284889276,3.26309273756545E-15));
#31985=CARTESIAN_POINT('Ctrl Pts',(2.6369636677978,-0.99226274488999,1.94109001754332E-16));
#31986=CARTESIAN_POINT('Ctrl Pts',(2.65826790515113,-0.90012905980095,-3.60822483003176E-16));
#31987=CARTESIAN_POINT('Ctrl Pts',(2.67972711543533,-0.807325168734929,
-9.19790693281215E-16));
#31988=CARTESIAN_POINT('Ctrl Pts',(2.6960170532411,-0.713217781371016,2.19518166871644E-16));
#31989=CARTESIAN_POINT('Ctrl Pts',(2.70721235053312,-0.618215105888531,
0.));
#31990=CARTESIAN_POINT('Ctrl Pts',(2.71292160521868,-0.56976668544991,-1.11947462410922E-16));
#31991=CARTESIAN_POINT('Ctrl Pts',(2.71730508064361,-0.521085594130936,
7.31925815782227E-16));
#31992=CARTESIAN_POINT('Ctrl Pts',(2.72036776812806,-0.472227710003176,
7.49400541621981E-16));
#31993=CARTESIAN_POINT('Ctrl Pts',(2.72142942533794,-0.455291497866967,
7.55458021783632E-16));
#31994=CARTESIAN_POINT('Ctrl Pts',(2.72233234751915,-0.438334056241388,
1.47771822505628E-15));
#31995=CARTESIAN_POINT('Ctrl Pts',(2.72307665503345,-0.421357761541496,
1.52655665885959E-15));
#31996=CARTESIAN_POINT('Ctrl Pts',(2.72371406196817,-0.40681967377542,1.56838071113613E-15));
#31997=CARTESIAN_POINT('Ctrl Pts',(2.72423475300693,-0.392276144899293,
-5.84163957766239E-16));
#31998=CARTESIAN_POINT('Ctrl Pts',(2.72463912967391,-0.377733018449256,
-5.82867087928207E-16));
#31999=CARTESIAN_POINT('Ctrl Pts',(2.7272335888012,-0.284425094826578,-5.74546440218005E-16));
#32000=CARTESIAN_POINT('Ctrl Pts',(2.72504700910767,-0.191075061278942,
2.51838167646803E-15));
#32001=CARTESIAN_POINT('Ctrl Pts',(2.71820565462271,-0.0980605230163078,
1.9151347174784E-15));
#32002=CARTESIAN_POINT('Ctrl Pts',(2.71136113957177,-0.00500301393752514,
1.31160907071961E-15));
#32003=CARTESIAN_POINT('Ctrl Pts',(2.69985717427859,0.0877196672682859,
-3.07238256336187E-16));
#32004=CARTESIAN_POINT('Ctrl Pts',(2.68376968445062,0.179716676654276,-1.04083408558608E-15));
#32005=CARTESIAN_POINT('Ctrl Pts',(2.6679263547778,0.270317445587206,-1.76329611625024E-15));
#32006=CARTESIAN_POINT('Ctrl Pts',(2.64763712143603,0.360215237891958,2.87404250511705E-16));
#32007=CARTESIAN_POINT('Ctrl Pts',(2.62293183221363,0.449011051883673,-1.38777878078145E-17));
#32008=CARTESIAN_POINT('Ctrl Pts',(2.6135041541326,0.482896036662513,-1.28848717445863E-16));
#32009=CARTESIAN_POINT('Ctrl Pts',(2.60343298467484,0.516620214186245,-4.06891175216909E-16));
#32010=CARTESIAN_POINT('Ctrl Pts',(2.592718513,0.550160020505481,-5.82867087928207E-16));
#32011=CARTESIAN_POINT('Ctrl Pts',(2.58640686113371,0.569917558494655,-6.86530500515623E-16));
#32012=CARTESIAN_POINT('Ctrl Pts',(2.57987196088238,0.589611101451674,-5.51406606223906E-16));
#32013=CARTESIAN_POINT('Ctrl Pts',(2.57311372784884,0.609235684372638,-7.21644966006352E-16));
#32014=CARTESIAN_POINT('Ctrl Pts',(2.56765136113167,0.625097325729763,-8.59240746715142E-16));
#32015=CARTESIAN_POINT('Ctrl Pts',(2.56204545311482,0.640906940190805,1.0191622183722E-15));
#32016=CARTESIAN_POINT('Ctrl Pts',(2.55629874325467,0.656655644997032,1.08246744900953E-15));
#32017=CARTESIAN_POINT('Ctrl Pts',(2.52550685343402,0.741039996219253,1.42166809325501E-15));
#32018=CARTESIAN_POINT('Ctrl Pts',(2.49065541114871,0.823737254187918,2.9255481979655E-15));
#32019=CARTESIAN_POINT('Ctrl Pts',(2.45179432548469,0.904376871334311,3.03229663600746E-15));
#32020=CARTESIAN_POINT('Ctrl Pts',(2.42326928916242,0.96356842424157,3.11065273492912E-15));
#32021=CARTESIAN_POINT('Ctrl Pts',(2.39258299461189,1.0216508685957,2.15271533017043E-15));
#32022=CARTESIAN_POINT('Ctrl Pts',(2.35974245541383,1.07846525592557,2.35922392732846E-15));
#32023=CARTESIAN_POINT('Ctrl Pts',(2.3470744452395,1.1003810117054,2.43888318609111E-15));
#32024=CARTESIAN_POINT('Ctrl Pts',(2.33408578165144,1.12210795602091,1.70584578534577E-15));
#32025=CARTESIAN_POINT('Ctrl Pts',(2.32077647825335,1.14363645354687,1.81799020282369E-15));
#32026=CARTESIAN_POINT('Ctrl Pts',(2.30811732205646,1.16411330381573,1.92465646889336E-15));
#32027=CARTESIAN_POINT('Ctrl Pts',(2.29516525813278,1.18441464884107,-2.41812693860714E-17));
#32028=CARTESIAN_POINT('Ctrl Pts',(2.28193698658913,1.20450712017389,0.));
#32029=CARTESIAN_POINT('Ctrl Pts',(2.23464326966583,1.27634172444316,8.6452875223902E-17));
#32030=CARTESIAN_POINT('Ctrl Pts',(2.18378846776941,1.34556635950281,1.71218066021624E-15));
#32031=CARTESIAN_POINT('Ctrl Pts',(2.1293995805356,1.4118263229903,7.73686670285656E-16));
#32032=CARTESIAN_POINT('Ctrl Pts',(2.09060596956493,1.45908713999166,1.04293112238207E-16));
#32033=CARTESIAN_POINT('Ctrl Pts',(2.05001367990221,1.50483902366414,-3.15793211228134E-16));
#32034=CARTESIAN_POINT('Ctrl Pts',(2.00762309288065,1.54893995061572,-2.67147415300428E-16));
#32035=CARTESIAN_POINT('Ctrl Pts',(1.9782489136182,1.57949929468088,-2.39592455248551E-16));
#32036=CARTESIAN_POINT('Ctrl Pts',(1.94801102665337,1.60926561951879,-8.19373708274163E-16));
#32037=CARTESIAN_POINT('Ctrl Pts',(1.91694983752522,1.63822102714876,-8.32667268468867E-16));
#32038=CARTESIAN_POINT('Ctrl Pts',(1.91346599666506,1.63598720337495,5.));
#32039=CARTESIAN_POINT('Ctrl Pts',(1.97511426248036,1.57805297138613,5.));
#32040=CARTESIAN_POINT('Ctrl Pts',(2.0333992327661,1.51697077668011,5.));
#32041=CARTESIAN_POINT('Ctrl Pts',(2.08832045660242,1.45312471107507,5.));
#32042=CARTESIAN_POINT('Ctrl Pts',(2.14469107178614,1.38759372425762,5.));
#32043=CARTESIAN_POINT('Ctrl Pts',(2.19751849836391,1.31915063045882,5.));
#32044=CARTESIAN_POINT('Ctrl Pts',(2.2467768545975,1.24816218982756,5.));
#32045=CARTESIAN_POINT('Ctrl Pts',(2.29674569779122,1.17614983436752,5.));
#32046=CARTESIAN_POINT('Ctrl Pts',(2.34304221736815,1.10151755915666,5.));
#32047=CARTESIAN_POINT('Ctrl Pts',(2.38560686750513,1.02460707565943,5.));
#32048=CARTESIAN_POINT('Ctrl Pts',(2.40516281592033,0.989271240805406,5.));
#32049=CARTESIAN_POINT('Ctrl Pts',(2.42393052938809,0.953453999419588,5.));
#32050=CARTESIAN_POINT('Ctrl Pts',(2.44190157522008,0.917186211225675,5.));
#32051=CARTESIAN_POINT('Ctrl Pts',(2.45212589418763,0.896552273823891,5.));
#32052=CARTESIAN_POINT('Ctrl Pts',(2.46209231213777,0.875772477886718,5.));
#32053=CARTESIAN_POINT('Ctrl Pts',(2.47179901297218,0.854852339979442,5.));
#32054=CARTESIAN_POINT('Ctrl Pts',(2.47986584870041,0.837466482643475,5.));
#32055=CARTESIAN_POINT('Ctrl Pts',(2.48775529546885,0.819978882487774,5.));
#32056=CARTESIAN_POINT('Ctrl Pts',(2.49545397654565,0.802421362463391,5.));
#32057=CARTESIAN_POINT('Ctrl Pts',(2.53207516621785,0.718903515111055,5.));
#32058=CARTESIAN_POINT('Ctrl Pts',(2.56443375074574,0.633702408588491,5.));
#32059=CARTESIAN_POINT('Ctrl Pts',(2.59250161927242,0.547215516795963,5.));
#32060=CARTESIAN_POINT('Ctrl Pts',(2.62102734916793,0.459317794443813,5.));
#32061=CARTESIAN_POINT('Ctrl Pts',(2.64512173324747,0.370091241926015,5.));
#32062=CARTESIAN_POINT('Ctrl Pts',(2.6647162612932,0.279916019321374,5.));
#32063=CARTESIAN_POINT('Ctrl Pts',(2.68327377745922,0.194513189135613,5.));
#32064=CARTESIAN_POINT('Ctrl Pts',(2.69779512543597,0.108258519972062,5.));
#32065=CARTESIAN_POINT('Ctrl Pts',(2.70818462605886,0.0214547457753918,
5.));
#32066=CARTESIAN_POINT('Ctrl Pts',(2.71280315092634,-0.0171328056643356,
5.));
#32067=CARTESIAN_POINT('Ctrl Pts',(2.71660465425308,-0.0558290637111655,
5.));
#32068=CARTESIAN_POINT('Ctrl Pts',(2.71957815680565,-0.0946081258455055,
5.));
#32069=CARTESIAN_POINT('Ctrl Pts',(2.72114193269849,-0.115002176780577,
5.));
#32070=CARTESIAN_POINT('Ctrl Pts',(2.72247667707736,-0.135419134083706,
5.));
#32071=CARTESIAN_POINT('Ctrl Pts',(2.72358060529281,-0.155855252406095,
5.));
#32072=CARTESIAN_POINT('Ctrl Pts',(2.72440760299952,-0.171164783180025,
5.));
#32073=CARTESIAN_POINT('Ctrl Pts',(2.72510503301269,-0.186486473786052,
5.));
#32074=CARTESIAN_POINT('Ctrl Pts',(2.72567165779787,-0.201800403224458,
5.));
#32075=CARTESIAN_POINT('Ctrl Pts',(2.72919576912562,-0.297045075921046,
5.));
#32076=CARTESIAN_POINT('Ctrl Pts',(2.72767362176579,-0.39214594976183,5.));
#32077=CARTESIAN_POINT('Ctrl Pts',(2.72104232884131,-0.48670474660219,5.));
#32078=CARTESIAN_POINT('Ctrl Pts',(2.71460574319996,-0.578487118597797,
5.));
#32079=CARTESIAN_POINT('Ctrl Pts',(2.70335577583384,-0.669759723511558,
5.));
#32080=CARTESIAN_POINT('Ctrl Pts',(2.68719094334706,-0.76017485193479,5.));
#32081=CARTESIAN_POINT('Ctrl Pts',(2.67098570391041,-0.850815989477801,
5.));
#32082=CARTESIAN_POINT('Ctrl Pts',(2.64984154989292,-0.940596245438192,
5.));
#32083=CARTESIAN_POINT('Ctrl Pts',(2.62403295621111,-1.02927270988445,5.));
#32084=CARTESIAN_POINT('Ctrl Pts',(2.60893641023223,-1.08114335185981,5.));
#32085=CARTESIAN_POINT('Ctrl Pts',(2.59224287435959,-1.13263631317645,5.));
#32086=CARTESIAN_POINT('Ctrl Pts',(2.57399925344803,-1.18370190437231,5.));
#32087=CARTESIAN_POINT('Ctrl Pts',(2.56913720383633,-1.19731123330153,5.));
#32088=CARTESIAN_POINT('Ctrl Pts',(2.5641650271584,-1.21089020050661,5.));
#32089=CARTESIAN_POINT('Ctrl Pts',(2.55908354497344,-1.22443784743359,5.));
#32090=CARTESIAN_POINT('Ctrl Pts',(2.55395835978812,-1.23810201013234,5.));
#32091=CARTESIAN_POINT('Ctrl Pts',(2.5487251194683,-1.25172589600239,5.));
#32092=CARTESIAN_POINT('Ctrl Pts',(2.54338628977321,-1.26530561093663,5.));
#32093=CARTESIAN_POINT('Ctrl Pts',(2.507474434899,-1.35665011521995,5.));
#32094=CARTESIAN_POINT('Ctrl Pts',(2.46677381849346,-1.44603954020521,5.));
#32095=CARTESIAN_POINT('Ctrl Pts',(2.42165814194307,-1.53319842974304,5.));
#32096=CARTESIAN_POINT('Ctrl Pts',(2.37698904164233,-1.61949457947533,5.));
#32097=CARTESIAN_POINT('Ctrl Pts',(2.32799127252537,-1.70360490076703,5.));
#32098=CARTESIAN_POINT('Ctrl Pts',(2.27497065048649,-1.78525830139829,5.));
#32099=CARTESIAN_POINT('Ctrl Pts',(2.22143189817264,-1.86770963870577,5.));
#32100=CARTESIAN_POINT('Ctrl Pts',(2.16379086711139,-1.94765663398949,5.));
#32101=CARTESIAN_POINT('Ctrl Pts',(2.10231135200038,-2.02480429723545,5.));
#32102=CARTESIAN_POINT('Ctrl Pts',(2.07897018428145,-2.05409399712484,5.));
#32103=CARTESIAN_POINT('Ctrl Pts',(2.05507524958568,-2.08297997370897,5.));
#32104=CARTESIAN_POINT('Ctrl Pts',(2.03063928040512,-2.11144510112202,5.));
#32105=CARTESIAN_POINT('Ctrl Pts',(2.01356866368511,-2.13133042985048,5.));
#32106=CARTESIAN_POINT('Ctrl Pts',(1.99623399133744,-2.1510103628177,5.));
#32107=CARTESIAN_POINT('Ctrl Pts',(1.97863935752325,-2.17047886391133,5.));
#32108=CARTESIAN_POINT('Ctrl Pts',(1.96848269337448,-2.18171723517703,5.));
#32109=CARTESIAN_POINT('Ctrl Pts',(1.95824201635888,-2.19288219327417,5.));
#32110=CARTESIAN_POINT('Ctrl Pts',(1.94792378478368,-2.20396685638102,5.));
#32111=CARTESIAN_POINT('Ctrl Pts',(1.87693652902952,-2.28022699933091,5.));
#32112=CARTESIAN_POINT('Ctrl Pts',(1.80220735563424,-2.35277244990143,5.));
#32113=CARTESIAN_POINT('Ctrl Pts',(1.7240709087608,-2.42127737465979,5.));
#32114=CARTESIAN_POINT('Ctrl Pts',(1.66546857360572,-2.47265606822857,5.));
#32115=CARTESIAN_POINT('Ctrl Pts',(1.60494837513541,-2.52176172516572,5.));
#32116=CARTESIAN_POINT('Ctrl Pts',(1.5426329601745,-2.56844590489654,5.));
#32117=CARTESIAN_POINT('Ctrl Pts',(1.50966649198766,-2.5931430448721,5.));
#32118=CARTESIAN_POINT('Ctrl Pts',(1.47619735041169,-2.61716230488521,5.));
#32119=CARTESIAN_POINT('Ctrl Pts',(1.44224214591351,-2.64048025951079,5.));
#32120=CARTESIAN_POINT('Ctrl Pts',(1.42523499995595,-2.65215952528491,5.));
#32121=CARTESIAN_POINT('Ctrl Pts',(1.40811304383442,-2.66365787868399,5.));
#32122=CARTESIAN_POINT('Ctrl Pts',(1.39088369966999,-2.6749695061669,5.));
#32123=CARTESIAN_POINT('Ctrl Pts',(1.30563891492228,-2.73093549307415,5.));
#32124=CARTESIAN_POINT('Ctrl Pts',(1.2177306352799,-2.78235921066159,5.));
#32125=CARTESIAN_POINT('Ctrl Pts',(1.12744207813993,-2.82892525415745,5.));
#32126=CARTESIAN_POINT('Ctrl Pts',(1.06580281768531,-2.86071551168622,5.));
#32127=CARTESIAN_POINT('Ctrl Pts',(1.00305327491768,-2.89024121467184,5.));
#32128=CARTESIAN_POINT('Ctrl Pts',(0.939273877630842,-2.91739189131414,
5.));
#32129=CARTESIAN_POINT('Ctrl Pts',(0.891985416295931,-2.93752243153926,
5.));
#32130=CARTESIAN_POINT('Ctrl Pts',(0.84413064869809,-2.95634718738556,5.));
#32131=CARTESIAN_POINT('Ctrl Pts',(0.795759619474682,-2.97387964574988,
5.));
#32132=CARTESIAN_POINT('Ctrl Pts',(-2.51589013302272,-0.00197902614912163,
3.38741669750803));
#32133=CARTESIAN_POINT('Ctrl Pts',(-2.51781607531079,-0.253199548871946,
3.40327713660639));
#32134=CARTESIAN_POINT('Ctrl Pts',(-2.48311008876547,-0.503899930938732,
3.41913757570475));
#32135=CARTESIAN_POINT('Ctrl Pts',(-2.40953623658284,-0.742620570455294,
3.43499801480311));
#32136=CARTESIAN_POINT('Ctrl Pts',(-2.16754372508865,-1.52779907325704,
3.48716474764301));
#32137=CARTESIAN_POINT('Ctrl Pts',(-1.50506907192147,-2.18337777113987,
3.5393314804829));
#32138=CARTESIAN_POINT('Ctrl Pts',(-0.717403027393835,-2.41715816749602,
3.5914982133228));
#32139=CARTESIAN_POINT('Ctrl Pts',(0.0702630171338087,-2.65093856385218,
3.64366494616269));
#32140=CARTESIAN_POINT('Ctrl Pts',(0.983120453021916,-2.46292065868166,
3.69583167900259));
#32141=CARTESIAN_POINT('Ctrl Pts',(1.61427619242997,-1.93687739549307,3.74799841184249));
#32142=CARTESIAN_POINT('Ctrl Pts',(2.24543193183803,-1.41083413230447,3.80016514468238));
#32143=CARTESIAN_POINT('Ctrl Pts',(2.59488597476604,-0.546765511097805,
3.85233187752228));
#32144=CARTESIAN_POINT('Ctrl Pts',(2.50687015370919,0.270115932309816,3.90449861036218));
#32145=CARTESIAN_POINT('Ctrl Pts',(2.41885433265234,1.08699737571744,3.95666534320207));
#32146=CARTESIAN_POINT('Ctrl Pts',(1.89336864761064,1.85669164132601,4.00883207604197));
#32147=CARTESIAN_POINT('Ctrl Pts',(1.16464828769536,2.23624130185117,4.06099880888186));
#32148=CARTESIAN_POINT('Ctrl Pts',(0.435927927780085,2.61579096237633,4.11316554172176));
#32149=CARTESIAN_POINT('Ctrl Pts',(-0.496027107008767,2.60519601781808,
4.16533227456166));
#32150=CARTESIAN_POINT('Ctrl Pts',(-1.21582191903011,2.20894048902741,4.21749900740156));
#32151=CARTESIAN_POINT('Ctrl Pts',(-1.93561673105145,1.81268496023674,4.26966574024145));
#32152=CARTESIAN_POINT('Ctrl Pts',(-2.44325132030528,1.03076884721365,4.32183247308135));
#32153=CARTESIAN_POINT('Ctrl Pts',(-2.51242976891092,0.212180128913875,
4.37399920592124));
#32154=CARTESIAN_POINT('Ctrl Pts',(-2.51836075980379,0.141998702022978,
4.37847170311684));
#32155=CARTESIAN_POINT('Ctrl Pts',(-2.52106890854963,0.0715477156323498,
4.38294420031243));
#32156=CARTESIAN_POINT('Ctrl Pts',(-2.52065797473119,0.00106685237120291,
4.38741669750802));
#32157=CARTESIAN_POINT('Ctrl Pts',(-0.793799282532885,-2.96922295374569,
5.));
#32158=CARTESIAN_POINT('Ctrl Pts',(-1.76703113798775,-2.70903678361534,
4.9478332671601));
#32159=CARTESIAN_POINT('Ctrl Pts',(-3.42227762319113,-1.16284338723151,
4.84349980148031));
#32160=CARTESIAN_POINT('Ctrl Pts',(-2.86382437134345,2.21031103269041,4.68699960296062));
#32161=CARTESIAN_POINT('Ctrl Pts',(0.252054090990421,3.60562829022214,4.53049940444094));
#32162=CARTESIAN_POINT('Ctrl Pts',(3.14100203598835,1.79029184281612,4.37399920592124));
#32163=CARTESIAN_POINT('Ctrl Pts',(3.23098071080095,-1.62294021205589,4.21749900740156));
#32164=CARTESIAN_POINT('Ctrl Pts',(0.440018754334274,-3.58837598279832,
4.06099880888186));
#32165=CARTESIAN_POINT('Ctrl Pts',(-2.74289544065113,-2.35537722830823,
3.90449861036218));
#32166=CARTESIAN_POINT('Ctrl Pts',(-3.48074999950888,0.977649265989379,
3.74799841184248));
#32167=CARTESIAN_POINT('Ctrl Pts',(-1.11551737463701,3.43898632522653,3.5914982133228));
#32168=CARTESIAN_POINT('Ctrl Pts',(2.24412684766706,2.83462531411003,3.43499801480311));
#32169=CARTESIAN_POINT('Ctrl Pts',(3.60321095550619,-0.296771509319279,
3.27849781628342));
#32170=CARTESIAN_POINT('Ctrl Pts',(1.75011009124083,-3.16358418358746,3.12199761776373));
#32171=CARTESIAN_POINT('Ctrl Pts',(-1.66316409145381,-3.2101505430571,2.96549741924404));
#32172=CARTESIAN_POINT('Ctrl Pts',(-3.59377214139091,-0.394942236718185,
2.80899722072435));
#32173=CARTESIAN_POINT('Ctrl Pts',(-2.3206200405613,2.77234451758071,2.65249702220466));
#32174=CARTESIAN_POINT('Ctrl Pts',(1.02130620401276,3.46815644429995,2.49599682368497));
#32175=CARTESIAN_POINT('Ctrl Pts',(3.45276382958855,1.07219267437738,2.33949662516528));
#32176=CARTESIAN_POINT('Ctrl Pts',(2.8061681927767,-2.27960425476498,2.18299642664559));
#32177=CARTESIAN_POINT('Ctrl Pts',(-0.34205648942751,-3.59919002761108,
2.02649622812591));
#32178=CARTESIAN_POINT('Ctrl Pts',(-3.18534629574052,-1.71018903949051,
1.86999602960622));
#32179=CARTESIAN_POINT('Ctrl Pts',(-3.18897927637007,1.7034061403768,1.71349583108653));
#32180=CARTESIAN_POINT('Ctrl Pts',(-0.349716256635896,3.59845088308181,
1.55699563256684));
#32181=CARTESIAN_POINT('Ctrl Pts',(2.8013094644448,2.28557822072128,1.40049543404715));
#32182=CARTESIAN_POINT('Ctrl Pts',(3.45503873870173,-1.0648536490447,1.24399523552746));
#32183=CARTESIAN_POINT('Ctrl Pts',(1.02868455419652,-3.46595066989846,1.08749503700777));
#32184=CARTESIAN_POINT('Ctrl Pts',(-2.31471172988138,-2.77732393751975,
0.930994838488083));
#32185=CARTESIAN_POINT('Ctrl Pts',(-3.5946088997546,0.387381135037168,0.774494639968393));
#32186=CARTESIAN_POINT('Ctrl Pts',(-1.66998478533906,3.20643252148329,0.617994441448703));
#32187=CARTESIAN_POINT('Ctrl Pts',(1.74335679702331,3.1676297706248,0.461494242929015));
#32188=CARTESIAN_POINT('Ctrl Pts',(3.60260150316633,0.3038109312067,0.304994044409326));
#32189=CARTESIAN_POINT('Ctrl Pts',(2.25009578791265,-2.82863139649778,0.148493845889636));
#32190=CARTESIAN_POINT('Ctrl Pts',(-1.10807133015233,-3.44371061769541,
-0.00800635263005217));
#32191=CARTESIAN_POINT('Ctrl Pts',(-3.47898841388462,-0.980218592702346,
-0.164506551149742));
#32192=CARTESIAN_POINT('Ctrl Pts',(-2.99072467884965,1.23160270904172,-0.268840016829535));
#32193=CARTESIAN_POINT('Ctrl Pts',(-2.33606265769614,1.99730155693066,-0.321006749669431));
#32194=CARTESIAN_POINT('Ctrl Pts',(-0.745932854346964,-2.79017756984215,
5.10700224988981));
#32195=CARTESIAN_POINT('Ctrl Pts',(-1.66047842254703,-2.54568073441083,
5.05483551704991));
#32196=CARTESIAN_POINT('Ctrl Pts',(-3.21591285354802,-1.09272344543869,
4.95050205137012));
#32197=CARTESIAN_POINT('Ctrl Pts',(-2.69113456596771,2.07702835450855,4.79400185285043));
#32198=CARTESIAN_POINT('Ctrl Pts',(0.236855124059054,3.38820739879938,4.63750165433075));
#32199=CARTESIAN_POINT('Ctrl Pts',(2.95159830169959,1.68233649716179,4.48100145581105));
#32200=CARTESIAN_POINT('Ctrl Pts',(3.03615122485059,-1.52507623961371,4.32450125729137));
#32201=CARTESIAN_POINT('Ctrl Pts',(0.413485439719026,-3.37199541271688,
4.16800105877167));
#32202=CARTESIAN_POINT('Ctrl Pts',(-2.57749770028975,-2.21334699795853,
4.01150086025199));
#32203=CARTESIAN_POINT('Ctrl Pts',(-3.2708593211588,0.918696607034865,3.85500066173229));
#32204=CARTESIAN_POINT('Ctrl Pts',(-1.04825121116451,3.231614013874,3.69850046321261));
#32205=CARTESIAN_POINT('Ctrl Pts',(2.10880506172238,2.66369622407748,3.54200026469292));
#32206=CARTESIAN_POINT('Ctrl Pts',(3.38593583037616,-0.278876063391019,
3.38550006617323));
#32207=CARTESIAN_POINT('Ctrl Pts',(1.64457772198429,-2.97281873636934,3.22899986765354));
#32208=CARTESIAN_POINT('Ctrl Pts',(-1.56287460228854,-3.01657712491928,
3.07249966913385));
#32209=CARTESIAN_POINT('Ctrl Pts',(-3.37706618069319,-0.371127054936794,
2.91599947061416));
#32210=CARTESIAN_POINT('Ctrl Pts',(-2.18068568314553,2.60517098558408,2.75949927209447));
#32211=CARTESIAN_POINT('Ctrl Pts',(0.95972101346657,3.25902516258738,2.60299907357479));
#32212=CARTESIAN_POINT('Ctrl Pts',(3.24456072897023,1.00753900842068,2.44649887505509));
#32213=CARTESIAN_POINT('Ctrl Pts',(2.63695507904276,-2.14214316635878,2.28999867653541));
#32214=CARTESIAN_POINT('Ctrl Pts',(-0.321430340290076,-3.38215736611206,
2.13349847801571));
#32215=CARTESIAN_POINT('Ctrl Pts',(-2.99326858407285,-1.60706392632346,
1.97699827949603));
#32216=CARTESIAN_POINT('Ctrl Pts',(-2.9966824944535,1.60069003885849,1.82049808097634));
#32217=CARTESIAN_POINT('Ctrl Pts',(-0.32862822033748,3.38146279230653,1.66399788245665));
#32218=CARTESIAN_POINT('Ctrl Pts',(2.63238933405802,2.1477568996735,1.50749768393696));
#32219=CARTESIAN_POINT('Ctrl Pts',(3.246698460114,-1.00064252937995,1.35099748541727));
#32220=CARTESIAN_POINT('Ctrl Pts',(0.96665444605344,-3.25695239730331,1.19449728689758));
#32221=CARTESIAN_POINT('Ctrl Pts',(-2.17513364606662,-2.60985014442166,
1.03799708837789));
#32222=CARTESIAN_POINT('Ctrl Pts',(-3.37785248217816,0.364021890844269,
0.881496889858204));
#32223=CARTESIAN_POINT('Ctrl Pts',(-1.56928400548455,3.01308330159882,0.724996691338513));
#32224=CARTESIAN_POINT('Ctrl Pts',(1.63823165422791,2.9766203728191,0.568496492818826));
#32225=CARTESIAN_POINT('Ctrl Pts',(3.38536312826686,0.285491005199331,0.411996294299136));
#32226=CARTESIAN_POINT('Ctrl Pts',(2.11441407237884,-2.65806374219999,0.255496095779446));
#32227=CARTESIAN_POINT('Ctrl Pts',(-1.04125416627134,-3.2360534295344,0.0989958972597585));
#32228=CARTESIAN_POINT('Ctrl Pts',(-3.26920395988323,-0.921111002274222,
-0.0575043012599318));
#32229=CARTESIAN_POINT('Ctrl Pts',(-2.81038273194434,1.15733655143344,-0.161837766939724));
#32230=CARTESIAN_POINT('Ctrl Pts',(-2.19519710401911,1.87686343907876,-0.214004499779621));
#32231=CARTESIAN_POINT('Ctrl Pts',(-0.698066426161043,-2.61113218593861,
5.21400449977962));
#32232=CARTESIAN_POINT('Ctrl Pts',(-1.55392570710631,-2.38232468520633,
5.16183776693972));
#32233=CARTESIAN_POINT('Ctrl Pts',(-3.00954808390491,-1.02260350364586,
5.05750430125993));
#32234=CARTESIAN_POINT('Ctrl Pts',(-2.51844476059198,1.94374567632669,4.90100410274025));
#32235=CARTESIAN_POINT('Ctrl Pts',(0.221656157127689,3.17078650737663,4.74450390422055));
#32236=CARTESIAN_POINT('Ctrl Pts',(2.76219456741083,1.57438115150745,4.58800370570087));
#32237=CARTESIAN_POINT('Ctrl Pts',(2.84132173890023,-1.42721226717154,4.43150350718117));
#32238=CARTESIAN_POINT('Ctrl Pts',(0.386952125103784,-3.15561484263544,
4.27500330866149));
#32239=CARTESIAN_POINT('Ctrl Pts',(-2.41209995992838,-2.07131676760884,
4.11850311014179));
#32240=CARTESIAN_POINT('Ctrl Pts',(-3.06096864280872,0.859743948080353,
3.96200291162211));
#32241=CARTESIAN_POINT('Ctrl Pts',(-0.98098504769201,3.02424170252148,3.80550271310242));
#32242=CARTESIAN_POINT('Ctrl Pts',(1.9734832757777,2.49276713404493,3.64900251458273));
#32243=CARTESIAN_POINT('Ctrl Pts',(3.16866070524613,-0.260980617462761,
3.49250231606304));
#32244=CARTESIAN_POINT('Ctrl Pts',(1.53904535272775,-2.78205328915123,3.33600211754335));
#32245=CARTESIAN_POINT('Ctrl Pts',(-1.46258511312328,-2.82300370678147,
3.17950191902366));
#32246=CARTESIAN_POINT('Ctrl Pts',(-3.16036021999547,-0.347311873155402,
3.02300172050397));
#32247=CARTESIAN_POINT('Ctrl Pts',(-2.04075132572976,2.43799745358745,2.86650152198428));
#32248=CARTESIAN_POINT('Ctrl Pts',(0.898135822920388,3.04989388087481,2.7100013234646));
#32249=CARTESIAN_POINT('Ctrl Pts',(3.03635762835191,0.942885342463967,2.5535011249449));
#32250=CARTESIAN_POINT('Ctrl Pts',(2.46774196530881,-2.00468207795258,2.39700092642522));
#32251=CARTESIAN_POINT('Ctrl Pts',(-0.300804191152645,-3.16512470461303,
2.24050072790553));
#32252=CARTESIAN_POINT('Ctrl Pts',(-2.80119087240519,-1.50393881315642,
2.08400052938584));
#32253=CARTESIAN_POINT('Ctrl Pts',(-2.80438571253693,1.49797393734019,1.92750033086615));
#32254=CARTESIAN_POINT('Ctrl Pts',(-0.307540184039062,3.16447470153125,
1.77100013234646));
#32255=CARTESIAN_POINT('Ctrl Pts',(2.46346920367124,2.00993557862573,1.61449993382677));
#32256=CARTESIAN_POINT('Ctrl Pts',(3.03835818152627,-0.936431409715195,
1.45799973530708));
#32257=CARTESIAN_POINT('Ctrl Pts',(0.904624337910361,-3.04795412470817,
1.30149953678739));
#32258=CARTESIAN_POINT('Ctrl Pts',(-2.03555556225185,-2.44237635132356,
1.1449993382677));
#32259=CARTESIAN_POINT('Ctrl Pts',(-3.16109606460172,0.340662646651362,
0.988499139748014));
#32260=CARTESIAN_POINT('Ctrl Pts',(-1.46858322563004,2.81973408171437,0.831998941228325));
#32261=CARTESIAN_POINT('Ctrl Pts',(1.53310651143252,2.78561097501341,0.675498742708636));
#32262=CARTESIAN_POINT('Ctrl Pts',(3.1681247533674,0.267171079191969,0.518998544188947));
#32263=CARTESIAN_POINT('Ctrl Pts',(1.97873235684504,-2.4874960879022,0.362498345669256));
#32264=CARTESIAN_POINT('Ctrl Pts',(-0.974437002390344,-3.02839624137338,
0.205998147149569));
#32265=CARTESIAN_POINT('Ctrl Pts',(-3.05941950588183,-0.862003411846101,
0.0494979486298786));
#32266=CARTESIAN_POINT('Ctrl Pts',(-2.63004078503903,1.08307039382515,-0.0548355170499138));
#32267=CARTESIAN_POINT('Ctrl Pts',(-2.05433155034208,1.75642532122686,-0.10700224988981));
#32268=CARTESIAN_POINT('Ctrl Pts',(-0.650199997975122,-2.43208680203507,
5.32100674966943));
#32269=CARTESIAN_POINT('Ctrl Pts',(-1.44737299166558,-2.21896863600183,
5.26884001682953));
#32270=CARTESIAN_POINT('Ctrl Pts',(-2.80318331426181,-0.952483561853041,
5.16450655114974));
#32271=CARTESIAN_POINT('Ctrl Pts',(-2.34575495521625,1.81046299814482,5.00800635263005));
#32272=CARTESIAN_POINT('Ctrl Pts',(0.206457190196319,2.95336561595388,4.85150615411036));
#32273=CARTESIAN_POINT('Ctrl Pts',(2.57279083312207,1.46642580585312,4.69500595559068));
#32274=CARTESIAN_POINT('Ctrl Pts',(2.64649225294986,-1.32934829472936,4.53850575707098));
#32275=CARTESIAN_POINT('Ctrl Pts',(0.360418810488541,-2.93923427255401,
4.3820055585513));
#32276=CARTESIAN_POINT('Ctrl Pts',(-2.24670221956701,-1.92928653725914,
4.22550536003161));
#32277=CARTESIAN_POINT('Ctrl Pts',(-2.85107796445863,0.800791289125838,
4.06900516151192));
#32278=CARTESIAN_POINT('Ctrl Pts',(-0.913718884219513,2.81686939116895,
3.91250496299223));
#32279=CARTESIAN_POINT('Ctrl Pts',(1.83816148983303,2.32183804401237,3.75600476447254));
#32280=CARTESIAN_POINT('Ctrl Pts',(2.9513855801161,-0.243085171534501,3.59950456595285));
#32281=CARTESIAN_POINT('Ctrl Pts',(1.43351298347121,-2.59128784193311,3.44300436743316));
#32282=CARTESIAN_POINT('Ctrl Pts',(-1.36229562395802,-2.62943028864365,
3.28650416891347));
#32283=CARTESIAN_POINT('Ctrl Pts',(-2.94365425929774,-0.323496691374012,
3.13000397039378));
#32284=CARTESIAN_POINT('Ctrl Pts',(-1.90081696831399,2.27082392159083,2.97350377187409));
#32285=CARTESIAN_POINT('Ctrl Pts',(0.836550632374203,2.84076259916223,2.81700357335441));
#32286=CARTESIAN_POINT('Ctrl Pts',(2.82815452773359,0.878231676507261,2.66050337483472));
#32287=CARTESIAN_POINT('Ctrl Pts',(2.29852885157487,-1.86722098954639,2.50400317631502));
#32288=CARTESIAN_POINT('Ctrl Pts',(-0.280178042015212,-2.948092043114,2.34750297779534));
#32289=CARTESIAN_POINT('Ctrl Pts',(-2.60911316073752,-1.40081369998938,
2.19100277927565));
#32290=CARTESIAN_POINT('Ctrl Pts',(-2.61208893062035,1.39525783582189,2.03450258075596));
#32291=CARTESIAN_POINT('Ctrl Pts',(-0.286452147740644,2.94748661075597,
1.87800238223627));
#32292=CARTESIAN_POINT('Ctrl Pts',(2.29454907328446,1.87211425757795,1.72150218371658));
#32293=CARTESIAN_POINT('Ctrl Pts',(2.83001790293854,-0.872220290050442,
1.56500198519689));
#32294=CARTESIAN_POINT('Ctrl Pts',(0.842594229767281,-2.83895585211302,
1.4085017866772));
#32295=CARTESIAN_POINT('Ctrl Pts',(-1.89597747843709,-2.27490255822547,
1.25200158815751));
#32296=CARTESIAN_POINT('Ctrl Pts',(-2.94433964702528,0.317303402458459,
1.09550138963782));
#32297=CARTESIAN_POINT('Ctrl Pts',(-1.36788244577553,2.6263848618299,0.939001191118136));
#32298=CARTESIAN_POINT('Ctrl Pts',(1.42798136863712,2.59460157720772,0.782500992598445));
#32299=CARTESIAN_POINT('Ctrl Pts',(2.95088637846794,0.248851153184599,0.626000794078758));
#32300=CARTESIAN_POINT('Ctrl Pts',(1.84305064131124,-2.31692843360441,0.469500595559067));
#32301=CARTESIAN_POINT('Ctrl Pts',(-0.907619838509351,-2.82073905321236,
0.31300039703938));
#32302=CARTESIAN_POINT('Ctrl Pts',(-2.84963505188044,-0.802895821417979,
0.156500198519689));
#32303=CARTESIAN_POINT('Ctrl Pts',(-2.44969883813372,1.00880423621686,0.0521667328398966));
#32304=CARTESIAN_POINT('Ctrl Pts',(-1.91346599666505,1.63598720337496,0.));
#32305=CARTESIAN_POINT('Ctrl Pts',(-1.91346599666505,1.63598720337496,0.));
#32306=CARTESIAN_POINT('Ctrl Pts',(-1.97511445450674,1.57805279092849,-2.16023702375061E-17));
#32307=CARTESIAN_POINT('Ctrl Pts',(-2.03339962644492,1.51697042789119,-3.49443898869507E-17));
#32308=CARTESIAN_POINT('Ctrl Pts',(-2.08832105501608,1.45312420295415,-1.11022302462516E-16));
#32309=CARTESIAN_POINT('Ctrl Pts',(-2.1446918579957,1.38759307857242,-1.89107908253736E-16));
#32310=CARTESIAN_POINT('Ctrl Pts',(-2.19751947843796,1.31914985899599,-1.96056269520747E-15));
#32311=CARTESIAN_POINT('Ctrl Pts',(-2.2467780277058,1.24816130047737,-2.16493489801906E-15));
#32312=CARTESIAN_POINT('Ctrl Pts',(-2.29674689545117,1.17614907224947,-2.37225419030257E-15));
#32313=CARTESIAN_POINT('Ctrl Pts',(-2.34304346389473,1.10151695033136,8.04059381600243E-19));
#32314=CARTESIAN_POINT('Ctrl Pts',(-2.38560818063646,1.02460663863002,2.77555756156289E-16));
#32315=CARTESIAN_POINT('Ctrl Pts',(-2.40516403209366,0.989271113192736,
4.04706022549276E-16));
#32316=CARTESIAN_POINT('Ctrl Pts',(-2.42393166263322,0.953454191414296,
1.85001145283656E-16));
#32317=CARTESIAN_POINT('Ctrl Pts',(-2.44190263911885,0.917186731710372,
2.77555756156289E-16));
#32318=CARTESIAN_POINT('Ctrl Pts',(-2.45212691902149,0.896552980413291,
3.30213120022811E-16));
#32319=CARTESIAN_POINT('Ctrl Pts',(-2.46209330228438,0.875773373445736,
1.0101923078241E-15));
#32320=CARTESIAN_POINT('Ctrl Pts',(-2.47179997273461,0.85485342713836,9.99200722162641E-16));
#32321=CARTESIAN_POINT('Ctrl Pts',(-2.47986685205683,0.837467580657393,
9.90065994086157E-16));
#32322=CARTESIAN_POINT('Ctrl Pts',(-2.48775634234785,0.819979991507439,
-1.29538532938285E-15));
#32323=CARTESIAN_POINT('Ctrl Pts',(-2.49545506671926,0.802422482605945,
-1.22124532708767E-15));
#32324=CARTESIAN_POINT('Ctrl Pts',(-2.53207648579799,0.718904634655909,
-8.68574941246235E-16));
#32325=CARTESIAN_POINT('Ctrl Pts',(-2.56443528935485,0.633703528135737,
-2.73580965033665E-16));
#32326=CARTESIAN_POINT('Ctrl Pts',(-2.59250335927894,0.547216632073775,
-2.22044604925031E-16));
#32327=CARTESIAN_POINT('Ctrl Pts',(-2.62102926303655,0.45931900035097,-1.696676067042E-16));
#32328=CARTESIAN_POINT('Ctrl Pts',(-2.64512381235207,0.370092536921413,
8.62583150244892E-16));
#32329=CARTESIAN_POINT('Ctrl Pts',(-2.6647184895653,0.279917395525893,9.71445146547012E-16));
#32330=CARTESIAN_POINT('Ctrl Pts',(-2.68327611608723,0.194514784532604,
1.07454560836236E-15));
#32331=CARTESIAN_POINT('Ctrl Pts',(-2.69779757345701,0.108260330337431,
1.58880599429527E-15));
#32332=CARTESIAN_POINT('Ctrl Pts',(-2.70818717658801,0.0214567600039818,
1.52655665885959E-15));
#32333=CARTESIAN_POINT('Ctrl Pts',(-2.71280574576047,-0.0171306902524466,
1.49888448909292E-15));
#32334=CARTESIAN_POINT('Ctrl Pts',(-2.71660729247955,-0.0558268492504973,
1.27797020542778E-15));
#32335=CARTESIAN_POINT('Ctrl Pts',(-2.71958083700161,-0.0946058150986653,
1.2490009027033E-15));
#32336=CARTESIAN_POINT('Ctrl Pts',(-2.72114459889708,-0.114999345005228,
1.23376619160252E-15));
#32337=CARTESIAN_POINT('Ctrl Pts',(-2.72247933944975,-0.135415780987334,
2.7744501595987E-15));
#32338=CARTESIAN_POINT('Ctrl Pts',(-2.72358327406089,-0.155851378047186,
2.83106871279415E-15));
#32339=CARTESIAN_POINT('Ctrl Pts',(-2.72441031908349,-0.171161305520925,
2.87348616409501E-15));
#32340=CARTESIAN_POINT('Ctrl Pts',(-2.72510778883702,-0.186483394270956,
-3.27116286657501E-16));
#32341=CARTESIAN_POINT('Ctrl Pts',(-2.72567444563692,-0.201797722043239,
-3.05311331771918E-16));
#32342=CARTESIAN_POINT('Ctrl Pts',(-2.72919865876058,-0.297042242048632,
-1.69699603154258E-16));
#32343=CARTESIAN_POINT('Ctrl Pts',(-2.7276765940473,-0.392142984842673,
1.65684655347014E-15));
#32344=CARTESIAN_POINT('Ctrl Pts',(-2.72104535728848,-0.486701680153984,
1.80411241501588E-15));
#32345=CARTESIAN_POINT('Ctrl Pts',(-2.71460882823241,-0.578483924102048,
1.94705422681979E-15));
#32346=CARTESIAN_POINT('Ctrl Pts',(-2.70335889560743,-0.669756429091281,
-1.44907627993903E-16));
#32347=CARTESIAN_POINT('Ctrl Pts',(-2.68719406942169,-0.760171493259568,
-2.4980018054066E-16));
#32348=CARTESIAN_POINT('Ctrl Pts',(-2.67098885106311,-0.850812483822458,
-3.27199259771174E-16));
#32349=CARTESIAN_POINT('Ctrl Pts',(-2.64984469854827,-0.940592630196976,
2.00672834831372E-15));
#32350=CARTESIAN_POINT('Ctrl Pts',(-2.62403609171522,-1.02926901742914,
1.97064586870965E-15));
#32351=CARTESIAN_POINT('Ctrl Pts',(-2.60893951244934,-1.08113970217868,
1.94953965336933E-15));
#32352=CARTESIAN_POINT('Ctrl Pts',(-2.59224593286086,-1.13263271607333,
1.51263892527377E-15));
#32353=CARTESIAN_POINT('Ctrl Pts',(-2.57400225902127,-1.18369836845093,
1.4432899320127E-15));
#32354=CARTESIAN_POINT('Ctrl Pts',(-2.56914004859136,-1.19730812434678,
1.42480739382975E-15));
#32355=CARTESIAN_POINT('Ctrl Pts',(-2.56416770379457,-1.21088751729747,
1.46101747209947E-15));
#32356=CARTESIAN_POINT('Ctrl Pts',(-2.55908604628673,-1.22443558863974,
1.41553435639707E-15));
#32357=CARTESIAN_POINT('Ctrl Pts',(-2.55396092950485,-1.23809952559165,
1.36966226068444E-15));
#32358=CARTESIAN_POINT('Ctrl Pts',(-2.54872776110117,-1.25172318692358,
7.2111001976691E-16));
#32359=CARTESIAN_POINT('Ctrl Pts',(-2.54338900633193,-1.26530267978209,
8.04911692853238E-16));
#32360=CARTESIAN_POINT('Ctrl Pts',(-2.50747702892334,-1.35664728387668,
1.36861688643376E-15));
#32361=CARTESIAN_POINT('Ctrl Pts',(-2.46677626545746,-1.44603683426546,
3.98698161417476E-15));
#32362=CARTESIAN_POINT('Ctrl Pts',(-2.42166042457756,-1.53319586749654,
3.8441472227646E-15));
#32363=CARTESIAN_POINT('Ctrl Pts',(-2.37699119409271,-1.6194920966769,3.70272677649499E-15));
#32364=CARTESIAN_POINT('Ctrl Pts',(-2.32799328414659,-1.70360251853944,
2.71566994649136E-15));
#32365=CARTESIAN_POINT('Ctrl Pts',(-2.27497251664925,-1.78525603476489,
3.10862446895044E-15));
#32366=CARTESIAN_POINT('Ctrl Pts',(-2.22143358365231,-1.86770754085407,
3.50541928807182E-15));
#32367=CARTESIAN_POINT('Ctrl Pts',(-2.16379236200239,-1.94765471708648,
2.12393071997628E-15));
#32368=CARTESIAN_POINT('Ctrl Pts',(-2.10231265300888,-2.02480256688325,
2.24820162486594E-15));
#32369=CARTESIAN_POINT('Ctrl Pts',(-2.07897144804811,-2.05409229196278,
2.29538195003625E-15));
#32370=CARTESIAN_POINT('Ctrl Pts',(-2.05507647736,-2.082978295804,3.52826900319682E-15));
#32371=CARTESIAN_POINT('Ctrl Pts',(-2.03064047373774,-2.11144345226609,
3.52495810318487E-15));
#32372=CARTESIAN_POINT('Ctrl Pts',(-2.01356997979656,-2.13132863023677,
3.52264517593754E-15));
#32373=CARTESIAN_POINT('Ctrl Pts',(-1.99623543552702,-2.15100841685411,
2.17794287054721E-15));
#32374=CARTESIAN_POINT('Ctrl Pts',(-1.97864093508987,-2.17047677606985,
2.02615701994091E-15));
#32375=CARTESIAN_POINT('Ctrl Pts',(-1.96848450504363,-2.18171489159328,
1.93853859740034E-15));
#32376=CARTESIAN_POINT('Ctrl Pts',(-1.95824406587573,-2.19287959838895,
2.78311917693584E-15));
#32377=CARTESIAN_POINT('Ctrl Pts',(-1.94792607632517,-2.20396401413293,
2.80331313717852E-15));
#32378=CARTESIAN_POINT('Ctrl Pts',(-1.87693852294064,-2.28022456377845,
2.94224716340022E-15));
#32379=CARTESIAN_POINT('Ctrl Pts',(-1.80220903731176,-2.35277040780027,
3.04985240962845E-15));
#32380=CARTESIAN_POINT('Ctrl Pts',(-1.72407227353766,-2.42127570338811,
3.40005801291454E-15));
#32381=CARTESIAN_POINT('Ctrl Pts',(-1.66546970070708,-2.472654675079,3.66271221537911E-15));
#32382=CARTESIAN_POINT('Ctrl Pts',(-1.60494926191777,-2.52176059742133,
2.66897608121856E-15));
#32383=CARTESIAN_POINT('Ctrl Pts',(-1.54263360799992,-2.56844502586205,
2.44249065417534E-15));
#32384=CARTESIAN_POINT('Ctrl Pts',(-1.50966712749181,-2.59314221193751,
2.32267441304543E-15));
#32385=CARTESIAN_POINT('Ctrl Pts',(-1.47619797745247,-2.61716151806854,
2.66421769654117E-15));
#32386=CARTESIAN_POINT('Ctrl Pts',(-1.44224276876128,-2.64047951847467,
2.55351295663786E-15));
#32387=CARTESIAN_POINT('Ctrl Pts',(-1.42523529016054,-2.65215903417213,
2.49806318714802E-15));
#32388=CARTESIAN_POINT('Ctrl Pts',(-1.40811299715223,-2.66365763094131,
1.70970381910793E-15));
#32389=CARTESIAN_POINT('Ctrl Pts',(-1.39088331342309,-2.6749694941009,1.85962356624714E-15));
#32390=CARTESIAN_POINT('Ctrl Pts',(-1.30563836789021,-2.73093564960753,
2.60136095853466E-15));
#32391=CARTESIAN_POINT('Ctrl Pts',(-1.21772994683618,-2.78235951649428,
1.84996893450162E-15));
#32392=CARTESIAN_POINT('Ctrl Pts',(-1.12744127475458,-2.82892568298919,
1.45369827286856E-15));
#32393=CARTESIAN_POINT('Ctrl Pts',(-1.06580182053759,-2.86071608395033,
1.18316702302153E-15));
#32394=CARTESIAN_POINT('Ctrl Pts',(-1.00305209219164,-2.89024190964375,
-1.85681498777599E-15));
#32395=CARTESIAN_POINT('Ctrl Pts',(-0.939272520240859,-2.91739268538644,
-2.72698530423554E-15));
#32396=CARTESIAN_POINT('Ctrl Pts',(-0.891984018423086,-2.93752326119295,
-3.3646306259368E-15));
#32397=CARTESIAN_POINT('Ctrl Pts',(-0.844129218472895,-2.95634804455667,
-1.21993627764454E-15));
#32398=CARTESIAN_POINT('Ctrl Pts',(-0.795758164394645,-2.97388052305262,
-1.30451205393456E-15));
#32399=CARTESIAN_POINT('Ctrl Pts',(-2.51644348201823,0.00207613456667446,
4.11258330249198));
#32400=CARTESIAN_POINT('Ctrl Pts',(-2.51833412820368,0.232035413192547,
4.09805725549862));
#32401=CARTESIAN_POINT('Ctrl Pts',(-2.489317966475,0.461526809188866,4.08353120850527));
#32402=CARTESIAN_POINT('Ctrl Pts',(-2.42745549360351,0.681791335068863,
4.06900516151192));
#32403=CARTESIAN_POINT('Ctrl Pts',(-2.20529160437893,1.47281732314021,4.01683842867202));
#32404=CARTESIAN_POINT('Ctrl Pts',(-1.55950524429922,2.14484335715458,3.96467169583213));
#32405=CARTESIAN_POINT('Ctrl Pts',(-0.777965335250612,2.39835114963567,
3.91250496299223));
#32406=CARTESIAN_POINT('Ctrl Pts',(0.00357457379799905,2.65185894211676,
3.86033823015234));
#32407=CARTESIAN_POINT('Ctrl Pts',(0.920868031815514,2.48684849306456,3.80817149731244));
#32408=CARTESIAN_POINT('Ctrl Pts',(1.56505210920478,1.97685606594732,3.75600476447254));
#32409=CARTESIAN_POINT('Ctrl Pts',(2.20923618659405,1.46686363883008,3.70383803163264));
#32410=CARTESIAN_POINT('Ctrl Pts',(2.58031088335508,0.611889233647789,3.65167129879275));
#32411=CARTESIAN_POINT('Ctrl Pts',(2.51286946562811,-0.206965080676461,
3.59950456595285));
#32412=CARTESIAN_POINT('Ctrl Pts',(2.44542804790114,-1.0258193950007,3.54733783311295));
#32413=CARTESIAN_POINT('Ctrl Pts',(1.93947051568617,-1.80855361846691,3.49517110027306));
#32414=CARTESIAN_POINT('Ctrl Pts',(1.22052364834049,-2.20627780465177,3.44300436743316));
#32415=CARTESIAN_POINT('Ctrl Pts',(0.501576780994809,-2.60400199083662,
3.39083763459327));
#32416=CARTESIAN_POINT('Ctrl Pts',(-0.430359421481595,-2.61671613974014,
3.33867090175337));
#32417=CARTESIAN_POINT('Ctrl Pts',(-1.15988729527642,-2.23875094798029,
3.28650416891347));
#32418=CARTESIAN_POINT('Ctrl Pts',(-1.88941516907125,-1.86078575622044,
3.23433743607358));
#32419=CARTESIAN_POINT('Ctrl Pts',(-2.4165347141845,-1.09214122379723,3.18217070323368));
#32420=CARTESIAN_POINT('Ctrl Pts',(-2.50628827157716,-0.275432188758138,
3.13000397039378));
#32421=CARTESIAN_POINT('Ctrl Pts',(-2.51627910181976,-0.18452101416286,
3.12419708109318));
#32422=CARTESIAN_POINT('Ctrl Pts',(-2.52085061170807,-0.0930142812830837,
3.11839019179258));
#32423=CARTESIAN_POINT('Ctrl Pts',(-2.52021651143941,-0.00144364612508765,
3.11258330249198));
#32424=CARTESIAN_POINT('Ctrl Pts',(-0.793799282532885,-2.96922295374569,
5.));
#32425=CARTESIAN_POINT('Ctrl Pts',(-0.886893974343616,-2.93516849963005,
5.));
#32426=CARTESIAN_POINT('Ctrl Pts',(-0.977926652176332,-2.89635378057927,
5.));
#32427=CARTESIAN_POINT('Ctrl Pts',(-1.06668684681747,-2.85310443912188,
5.));
#32428=CARTESIAN_POINT('Ctrl Pts',(-1.15738407105809,-2.80891125955214,
5.));
#32429=CARTESIAN_POINT('Ctrl Pts',(-1.2457092143346,-2.76008717620201,5.));
#32430=CARTESIAN_POINT('Ctrl Pts',(-1.33140881802392,-2.70693414934569,
5.));
#32431=CARTESIAN_POINT('Ctrl Pts',(-1.4129353161641,-2.65636938639935,5.));
#32432=CARTESIAN_POINT('Ctrl Pts',(-1.49208596169445,-2.60188611256442,
5.));
#32433=CARTESIAN_POINT('Ctrl Pts',(-1.56861084771671,-2.54371537355153,
5.));
#32434=CARTESIAN_POINT('Ctrl Pts',(-1.63557012298619,-2.49281597691525,
5.));
#32435=CARTESIAN_POINT('Ctrl Pts',(-1.70051877227587,-2.43909270266388,
5.));
#32436=CARTESIAN_POINT('Ctrl Pts',(-1.76326584581776,-2.38268809603059,
5.));
#32437=CARTESIAN_POINT('Ctrl Pts',(-1.77895171505325,-2.36858775263627,
5.));
#32438=CARTESIAN_POINT('Ctrl Pts',(-1.79450406853106,-2.35431573679482,
5.));
#32439=CARTESIAN_POINT('Ctrl Pts',(-1.80989576842494,-2.33989703960917,
5.));
#32440=CARTESIAN_POINT('Ctrl Pts',(-1.88231927767376,-2.27205185966276,
5.));
#32441=CARTESIAN_POINT('Ctrl Pts',(-1.95127665379114,-2.20088663840561,
5.));
#32442=CARTESIAN_POINT('Ctrl Pts',(-2.0165263629502,-2.1266887335995,5.));
#32443=CARTESIAN_POINT('Ctrl Pts',(-2.08140824110774,-2.05290910329586,
5.));
#32444=CARTESIAN_POINT('Ctrl Pts',(-2.14262462446156,-1.97613009459816,
5.));
#32445=CARTESIAN_POINT('Ctrl Pts',(-2.19989444056472,-1.89660745904738,
5.));
#32446=CARTESIAN_POINT('Ctrl Pts',(-2.25380452290626,-1.82175001891108,
5.));
#32447=CARTESIAN_POINT('Ctrl Pts',(-2.30421749508371,-1.74446069179507,
5.));
#32448=CARTESIAN_POINT('Ctrl Pts',(-2.35085748563793,-1.66494010874883,
5.));
#32449=CARTESIAN_POINT('Ctrl Pts',(-2.38695950989298,-1.6033866224853,5.));
#32450=CARTESIAN_POINT('Ctrl Pts',(-2.42080014316453,-1.54049593023453,
5.));
#32451=CARTESIAN_POINT('Ctrl Pts',(-2.45223267762586,-1.47635917633043,
5.));
#32452=CARTESIAN_POINT('Ctrl Pts',(-2.45885074786154,-1.46285528460488,
5.));
#32453=CARTESIAN_POINT('Ctrl Pts',(-2.46536230022247,-1.44929534936329,
5.));
#32454=CARTESIAN_POINT('Ctrl Pts',(-2.471759088022,-1.4356951550231,5.));
#32455=CARTESIAN_POINT('Ctrl Pts',(-2.51224453952186,-1.34961913912194,
5.));
#32456=CARTESIAN_POINT('Ctrl Pts',(-2.54820623907542,-1.26179296188141,
5.));
#32457=CARTESIAN_POINT('Ctrl Pts',(-2.57938608018177,-1.17245518793809,
5.));
#32458=CARTESIAN_POINT('Ctrl Pts',(-2.61056592128812,-1.08311741399478,
5.));
#32459=CARTESIAN_POINT('Ctrl Pts',(-2.63696435690728,-0.992267333350395,
5.));
#32460=CARTESIAN_POINT('Ctrl Pts',(-2.65826858221262,-0.900133621000477,
5.));
#32461=CARTESIAN_POINT('Ctrl Pts',(-2.67972778132943,-0.807329698287973,
5.));
#32462=CARTESIAN_POINT('Ctrl Pts',(-2.69601769794397,-0.713222227763925,
5.));
#32463=CARTESIAN_POINT('Ctrl Pts',(-2.70721296581232,-0.618219427263112,
5.));
#32464=CARTESIAN_POINT('Ctrl Pts',(-2.71292220509282,-0.569770946462525,
5.));
#32465=CARTESIAN_POINT('Ctrl Pts',(-2.7173056631566,-0.521089783925043,
5.));
#32466=CARTESIAN_POINT('Ctrl Pts',(-2.7203683315583,-0.472231818984886,
5.));
#32467=CARTESIAN_POINT('Ctrl Pts',(-2.72142997921888,-0.45529562564751,
5.));
#32468=CARTESIAN_POINT('Ctrl Pts',(-2.72233289252141,-0.438338201785387,
5.));
#32469=CARTESIAN_POINT('Ctrl Pts',(-2.72307719183649,-0.421361923846564,
5.));
#32470=CARTESIAN_POINT('Ctrl Pts',(-2.72371459453401,-0.40682378692649,
5.));
#32471=CARTESIAN_POINT('Ctrl Pts',(-2.72423528082335,-0.392280207970546,
5.));
#32472=CARTESIAN_POINT('Ctrl Pts',(-2.72463965223211,-0.3777370307415,5.));
#32473=CARTESIAN_POINT('Ctrl Pts',(-2.7272340736051,-0.284428925823235,
5.));
#32474=CARTESIAN_POINT('Ctrl Pts',(-2.72504745011893,-0.191078680030525,
5.));
#32475=CARTESIAN_POINT('Ctrl Pts',(-2.71820604758435,-0.0980639080872022,
5.));
#32476=CARTESIAN_POINT('Ctrl Pts',(-2.71136148545356,-0.00500617870656192,
5.));
#32477=CARTESIAN_POINT('Ctrl Pts',(-2.69985747016539,0.0877167443723885,
5.));
#32478=CARTESIAN_POINT('Ctrl Pts',(-2.68376992914425,0.179714008003965,
5.));
#32479=CARTESIAN_POINT('Ctrl Pts',(-2.66792655922036,0.27031496919411,5.));
#32480=CARTESIAN_POINT('Ctrl Pts',(-2.64763729016321,0.360212966671102,
5.));
#32481=CARTESIAN_POINT('Ctrl Pts',(-2.62293197139578,0.449008990638608,
5.));
#32482=CARTESIAN_POINT('Ctrl Pts',(-2.61350433154693,0.482893877607947,
5.));
#32483=CARTESIAN_POINT('Ctrl Pts',(-2.60343320797911,0.516617959708256,
5.));
#32484=CARTESIAN_POINT('Ctrl Pts',(-2.5927187899484,0.55015767290499,5.));
#32485=CARTESIAN_POINT('Ctrl Pts',(-2.58640692567121,0.569915919875281,
5.));
#32486=CARTESIAN_POINT('Ctrl Pts',(-2.57987179843875,0.589610167664632,
5.));
#32487=CARTESIAN_POINT('Ctrl Pts',(-2.57311332386527,0.609235450675716,
5.));
#32488=CARTESIAN_POINT('Ctrl Pts',(-2.5676510579122,0.625096798387423,5.));
#32489=CARTESIAN_POINT('Ctrl Pts',(-2.5620452571388,0.640906120496968,5.));
#32490=CARTESIAN_POINT('Ctrl Pts',(-2.55629866051782,0.656654535691256,
5.));
#32491=CARTESIAN_POINT('Ctrl Pts',(-2.52550674415446,0.741039070660769,
5.));
#32492=CARTESIAN_POINT('Ctrl Pts',(-2.4906552842231,0.823736510163055,5.));
#32493=CARTESIAN_POINT('Ctrl Pts',(-2.45179419129016,0.9043762990239,5.));
#32494=CARTESIAN_POINT('Ctrl Pts',(-2.42326911496468,0.963568049912018,
5.));
#32495=CARTESIAN_POINT('Ctrl Pts',(-2.39258278075448,1.0216506842635,5.));
#32496=CARTESIAN_POINT('Ctrl Pts',(-2.35974220291426,1.07846524994913,5.));
#32497=CARTESIAN_POINT('Ctrl Pts',(-2.34707421607123,1.10038100837762,5.));
#32498=CARTESIAN_POINT('Ctrl Pts',(-2.3340855779016,1.12210795474778,5.));
#32499=CARTESIAN_POINT('Ctrl Pts',(-2.32077630204861,1.14363645360599,5.));
#32500=CARTESIAN_POINT('Ctrl Pts',(-2.30811708022228,1.16411345368055,5.));
#32501=CARTESIAN_POINT('Ctrl Pts',(-2.29516494832623,1.18441494534906,5.));
#32502=CARTESIAN_POINT('Ctrl Pts',(-2.28193660666336,1.2045075595742,5.));
#32503=CARTESIAN_POINT('Ctrl Pts',(-2.23464292719215,1.27634223705079,5.));
#32504=CARTESIAN_POINT('Ctrl Pts',(-2.18378817877942,1.34556692931273,5.));
#32505=CARTESIAN_POINT('Ctrl Pts',(-2.12939936247367,1.41182692759809,5.));
#32506=CARTESIAN_POINT('Ctrl Pts',(-2.09060564520546,1.45908796055058,5.));
#32507=CARTESIAN_POINT('Ctrl Pts',(-2.0500132435823,1.504840036578,5.));
#32508=CARTESIAN_POINT('Ctrl Pts',(-2.00762253952656,1.54894112815615,5.));
#32509=CARTESIAN_POINT('Ctrl Pts',(-1.9782483512311,1.57950051132536,5.));
#32510=CARTESIAN_POINT('Ctrl Pts',(-1.94801045703336,1.60926686583501,5.));
#32511=CARTESIAN_POINT('Ctrl Pts',(-1.91694926235925,1.63822229446221,5.));
#32512=CARTESIAN_POINT('Origin',(0.,0.,5.));
#32513=CARTESIAN_POINT('',(2.88675134594813,-5.,5.));
#32514=CARTESIAN_POINT('',(5.77350269189626,0.,5.));
#32515=CARTESIAN_POINT('',(2.88675134594813,-5.,5.));
#32516=CARTESIAN_POINT('',(2.88675134594813,5.,5.));
#32517=CARTESIAN_POINT('',(5.77350269189626,0.,5.));
#32518=CARTESIAN_POINT('',(-2.88675134594813,5.,5.));
#32519=CARTESIAN_POINT('',(2.88675134594813,5.,5.));
#32520=CARTESIAN_POINT('',(-5.77350269189626,1.11022302462516E-15,5.));
#32521=CARTESIAN_POINT('',(-2.88675134594813,5.,5.));
#32522=CARTESIAN_POINT('',(-2.88675134594813,-5.,5.));
#32523=CARTESIAN_POINT('',(-5.77350269189626,7.07050159149938E-16,5.));
#32524=CARTESIAN_POINT('',(-2.88675134594813,-5.,5.));
#32525=CARTESIAN_POINT('Origin',(0.,0.,2.5));
#32526=CARTESIAN_POINT('Origin',(-2.88675134594813,-5.,0.));
#32527=CARTESIAN_POINT('',(-2.88675134594813,-5.,0.));
#32528=CARTESIAN_POINT('',(2.88675134594813,-5.,0.));
#32529=CARTESIAN_POINT('',(-2.88675134594813,-5.,0.));
#32530=CARTESIAN_POINT('',(2.88675134594813,-5.,0.));
#32531=CARTESIAN_POINT('',(-2.88675134594813,-5.,0.));
#32532=CARTESIAN_POINT('Origin',(-5.77350269189626,7.07050159149938E-16,
0.));
#32533=CARTESIAN_POINT('',(-5.77350269189626,7.07050159149938E-16,0.));
#32534=CARTESIAN_POINT('',(-5.77350269189626,7.07050159149938E-16,0.));
#32535=CARTESIAN_POINT('',(-5.77350269189626,7.07050159149938E-16,0.));
#32536=CARTESIAN_POINT('Origin',(-2.88675134594813,5.,0.));
#32537=CARTESIAN_POINT('',(-2.88675134594813,5.,0.));
#32538=CARTESIAN_POINT('',(-2.88675134594813,5.,0.));
#32539=CARTESIAN_POINT('',(-2.88675134594813,5.,0.));
#32540=CARTESIAN_POINT('Origin',(2.88675134594813,5.,0.));
#32541=CARTESIAN_POINT('',(2.88675134594813,5.,0.));
#32542=CARTESIAN_POINT('',(2.88675134594813,5.,0.));
#32543=CARTESIAN_POINT('',(2.88675134594813,5.,0.));
#32544=CARTESIAN_POINT('Origin',(5.77350269189626,0.,0.));
#32545=CARTESIAN_POINT('',(5.77350269189626,0.,0.));
#32546=CARTESIAN_POINT('',(5.77350269189626,0.,0.));
#32547=CARTESIAN_POINT('',(5.77350269189626,0.,0.));
#32548=CARTESIAN_POINT('Origin',(2.88675134594813,-5.,0.));
#32549=CARTESIAN_POINT('',(2.88675134594813,-5.,0.));
#32550=CARTESIAN_POINT('Origin',(0.,0.,0.));
#32606=UNCERTAINTY_MEASURE_WITH_UNIT(LENGTH_MEASURE(0.01),#32628,
'DISTANCE_ACCURACY_VALUE',
'Maximum model space distance between geometric entities at asserted c
onnectivities');
#32607=UNCERTAINTY_MEASURE_WITH_UNIT(LENGTH_MEASURE(0.01),#32628,
'DISTANCE_ACCURACY_VALUE',
'Maximum model space distance between geometric entities at asserted c
onnectivities');
#32626=(
GEOMETRIC_REPRESENTATION_CONTEXT(3)
GLOBAL_UNCERTAINTY_ASSIGNED_CONTEXT((#32606))
GLOBAL_UNIT_ASSIGNED_CONTEXT((#32628,#32630,#32631))
REPRESENTATION_CONTEXT('','3D')
);
#32627=(
GEOMETRIC_REPRESENTATION_CONTEXT(3)
GLOBAL_UNCERTAINTY_ASSIGNED_CONTEXT((#32607))
GLOBAL_UNIT_ASSIGNED_CONTEXT((#32628,#32630,#32631))
REPRESENTATION_CONTEXT('','3D')
);
#32628=(
LENGTH_UNIT()
NAMED_UNIT(*)
SI_UNIT(.MILLI.,.METRE.)
);
#32630=(
NAMED_UNIT(*)
PLANE_ANGLE_UNIT()
SI_UNIT($,.RADIAN.)
);
#32631=(
NAMED_UNIT(*)
SI_UNIT($,.STERADIAN.)
SOLID_ANGLE_UNIT()
);
#32650=SHAPE_DEFINITION_REPRESENTATION(#32669,#32725);
#32669=PRODUCT_DEFINITION_SHAPE('',$,#32745);
#32725=SHAPE_REPRESENTATION('',(#9467),#32626);
#32726=PRODUCT_DEFINITION_CONTEXT('part definition',#32785,'design');
#32745=PRODUCT_DEFINITION('Hex nut M6','Hex nut M6',#32764,#32726);
#32764=PRODUCT_DEFINITION_FORMATION('',$,#32805);
#32785=APPLICATION_CONTEXT(
'Core Data for Automotive Mechanical Design Process');
#32786=PRODUCT_CONTEXT('part definition',#32785,'mechanical');
#32805=PRODUCT('Hex nut M6','Hex nut M6',$,(#32786));
#32810=PRESENTATION_STYLE_ASSIGNMENT((#32817));
#32817=SURFACE_STYLE_USAGE(.BOTH.,#32824);
#32824=SURFACE_SIDE_STYLE('',(#32831));
#32831=SURFACE_STYLE_FILL_AREA(#32838);
#32838=FILL_AREA_STYLE('Gray',(#32845));
#32845=FILL_AREA_STYLE_COLOUR('Gray',#32852);
#32852=COLOUR_RGB('Gray',0.407843137254902,0.447058823529412,0.498039215686275);
ENDSEC;
END-ISO-10303-21;
